ISO-10303-21;
HEADER;
/* Generated by software containing ST-Developer
 * from STEP Tools, Inc. (www.steptools.com) 
 */

FILE_DESCRIPTION(
/* description */ ('Wheel Holder-Mirrored'),
/* implementation_level */ '2;1');

FILE_NAME(
/* name */ 'Hex flange nut M6x1.00.step',
/* time_stamp */ '2026-10-07T09:01:46-07:00',
/* author */ (''),
/* organization */ (''),
/* preprocessor_version */ 'ST-DEVELOPER v20.2',
/* originating_system */ 'Autodesk Translation Framework v15.15.0.0',
/* authorisation */ '');

FILE_SCHEMA (('AUTOMOTIVE_DESIGN { 1 0 10303 214 3 1 1 }'));
ENDSEC;

DATA;
#10=MECHANICAL_DESIGN_GEOMETRIC_PRESENTATION_REPRESENTATION('',(#202),#3832);
#84=(
BOUNDED_SURFACE()
B_SPLINE_SURFACE(3,2,((#3298,#3299,#3300),(#3301,#3302,#3303),(#3304,#3305,
#3306),(#3307,#3308,#3309),(#3310,#3311,#3312)),.UNSPECIFIED.,.F.,.F.,.F.)
B_SPLINE_SURFACE_WITH_KNOTS((4,1,4),(3,3),(0.0246620904109836,0.0279939304185144,
0.0313257704892837),(0.,1.00067047018092),.UNSPECIFIED.)
GEOMETRIC_REPRESENTATION_ITEM()
RATIONAL_B_SPLINE_SURFACE(((1.,0.802865969663045,1.00026434497797),(1.,
0.81108910405605,1.00025331824517),(1.,0.82686917993846,1.0002321581045),
(1.,0.81129221048254,1.00025304589156),(1.,0.802807804958138,1.00026442297338)))
REPRESENTATION_ITEM('')
SURFACE()
);
#85=(
BOUNDED_SURFACE()
B_SPLINE_SURFACE(3,2,((#3337,#3338,#3339),(#3340,#3341,#3342),(#3343,#3344,
#3345),(#3346,#3347,#3348),(#3349,#3350,#3351)),.UNSPECIFIED.,.F.,.F.,.F.)
B_SPLINE_SURFACE_WITH_KNOTS((4,1,4),(3,3),(0.024738817097226,0.0280688166766824,
0.0313988162601249),(0.,1.00066549850917),.UNSPECIFIED.)
GEOMETRIC_REPRESENTATION_ITEM()
RATIONAL_B_SPLINE_SURFACE(((1.,0.802880827397706,1.00026236503099),(1.,
0.811099228845429,1.00025142636317),(1.,0.82686120340028,1.00023044722203),
(1.,0.811301685281914,1.00025115689426),(1.,0.80282325859447,1.0002624416549)))
REPRESENTATION_ITEM('')
SURFACE()
);
#86=(
BOUNDED_SURFACE()
B_SPLINE_SURFACE(3,2,((#3364,#3365,#3366),(#3367,#3368,#3369),(#3370,#3371,
#3372),(#3373,#3374,#3375),(#3376,#3377,#3378)),.UNSPECIFIED.,.F.,.F.,.F.)
B_SPLINE_SURFACE_WITH_KNOTS((4,1,4),(3,3),(0.024738817096804,0.0280688166766824,
0.0313988162605461),(0.,1.00066549851789),.UNSPECIFIED.)
GEOMETRIC_REPRESENTATION_ITEM()
RATIONAL_B_SPLINE_SURFACE(((1.,0.802880827392752,1.00026236503443),(1.,
0.811099228842278,1.00025142636647),(1.,0.826861203399938,1.00023044722505),
(1.,0.811301685279444,1.00025115689755),(1.,0.802823258589269,1.00026244165835)))
REPRESENTATION_ITEM('')
SURFACE()
);
#87=(
BOUNDED_SURFACE()
B_SPLINE_SURFACE(3,2,((#3391,#3392,#3393),(#3394,#3395,#3396),(#3397,#3398,
#3399),(#3400,#3401,#3402),(#3403,#3404,#3405)),.UNSPECIFIED.,.F.,.F.,.F.)
B_SPLINE_SURFACE_WITH_KNOTS((4,1,4),(3,3),(0.0247388170968889,0.0280688166766824,
0.0313988162604618),(0.,1.00066549851781),.UNSPECIFIED.)
GEOMETRIC_REPRESENTATION_ITEM()
RATIONAL_B_SPLINE_SURFACE(((1.,0.802880827393329,1.00026236503441),(1.,
0.811099228842959,1.00025142636643),(1.,0.82686120340021,1.00023044722503),
(1.,0.811301685278279,1.00025115689751),(1.,0.802823258590303,1.0002624416583)))
REPRESENTATION_ITEM('')
SURFACE()
);
#88=(
BOUNDED_SURFACE()
B_SPLINE_SURFACE(3,2,((#3418,#3419,#3420),(#3421,#3422,#3423),(#3424,#3425,
#3426),(#3427,#3428,#3429),(#3430,#3431,#3432)),.UNSPECIFIED.,.F.,.F.,.F.)
B_SPLINE_SURFACE_WITH_KNOTS((4,1,4),(3,3),(0.0247388170974279,0.0280688166766824,
0.031398816259923),(0.,1.00066549852508),.UNSPECIFIED.)
GEOMETRIC_REPRESENTATION_ITEM()
RATIONAL_B_SPLINE_SURFACE(((1.,0.802880827396021,1.00026236503726),(1.,
0.811099228843575,1.00025142636918),(1.,0.826861203396443,1.00023044722754),
(1.,0.811301685279931,1.00025115690027),(1.,0.80282325859286,1.00026244166118)))
REPRESENTATION_ITEM('')
SURFACE()
);
#89=(
BOUNDED_SURFACE()
B_SPLINE_SURFACE(3,2,((#3445,#3446,#3447),(#3448,#3449,#3450),(#3451,#3452,
#3453),(#3454,#3455,#3456),(#3457,#3458,#3459)),.UNSPECIFIED.,.F.,.F.,.F.)
B_SPLINE_SURFACE_WITH_KNOTS((4,1,4),(3,3),(0.0246749646102296,0.0280029916911416,
0.031331018716321),(0.,1.00065966906838),.UNSPECIFIED.)
GEOMETRIC_REPRESENTATION_ITEM()
RATIONAL_B_SPLINE_SURFACE(((1.,0.802898366215555,1.00026004370227),(1.,
0.811111461933951,1.00024920785186),(1.,0.826851645151749,1.00022844122787),
(1.,0.811312849119053,1.00024894215407),(1.,0.802841584394648,1.00026011861669)))
REPRESENTATION_ITEM('')
SURFACE()
);
#92=TOROIDAL_SURFACE('',#1982,0.00653289983773083,0.000567100162269171);
#101=CONICAL_SURFACE('',#1973,0.005,1.0471975511966);
#102=CONICAL_SURFACE('',#1974,0.005,1.0471975511966);
#103=CONICAL_SURFACE('',#1975,0.005,1.0471975511966);
#104=CONICAL_SURFACE('',#1976,0.005,1.0471975511966);
#105=CONICAL_SURFACE('',#1977,0.005,1.0471975511966);
#106=CONICAL_SURFACE('',#1978,0.005,1.0471975511966);
#107=CONICAL_SURFACE('',#1979,0.00672685951651014,1.22173047639603);
#108=CONICAL_SURFACE('',#1984,0.003,0.785398163397448);
#109=CONICAL_SURFACE('',#1985,0.0024585,0.785398163397448);
#122=(
BOUNDED_CURVE()
B_SPLINE_CURVE(2,(#3088,#3089,#3090),.UNSPECIFIED.,.F.,.F.)
B_SPLINE_CURVE_WITH_KNOTS((3,3),(0.868406024324111,1.41937586994552),
 .UNSPECIFIED.)
CURVE()
GEOMETRIC_REPRESENTATION_ITEM()
RATIONAL_B_SPLINE_CURVE((1.77300211797113,1.91014430907105,1.91014430907105))
REPRESENTATION_ITEM('')
);
#123=(
BOUNDED_CURVE()
B_SPLINE_CURVE(2,(#3091,#3092,#3093),.UNSPECIFIED.,.F.,.F.)
B_SPLINE_CURVE_WITH_KNOTS((3,3),(1.41937586994552,1.97034571556692),
 .UNSPECIFIED.)
CURVE()
GEOMETRIC_REPRESENTATION_ITEM()
RATIONAL_B_SPLINE_CURVE((1.91014430907105,1.91014430907105,1.77300211797113))
REPRESENTATION_ITEM('')
);
#124=(
BOUNDED_CURVE()
B_SPLINE_CURVE(2,(#3115,#3116,#3117),.UNSPECIFIED.,.F.,.F.)
B_SPLINE_CURVE_WITH_KNOTS((3,3),(0.868406111432395,1.41937598717132),
 .UNSPECIFIED.)
CURVE()
GEOMETRIC_REPRESENTATION_ITEM()
RATIONAL_B_SPLINE_CURVE((1.7730022081019,1.91014440617345,1.91014440617345))
REPRESENTATION_ITEM('')
);
#125=(
BOUNDED_CURVE()
B_SPLINE_CURVE(2,(#3118,#3119,#3120),.UNSPECIFIED.,.F.,.F.)
B_SPLINE_CURVE_WITH_KNOTS((3,3),(1.41937598717132,1.97034586291024),
 .UNSPECIFIED.)
CURVE()
GEOMETRIC_REPRESENTATION_ITEM()
RATIONAL_B_SPLINE_CURVE((1.91014440617345,1.91014440617345,1.7730022081019))
REPRESENTATION_ITEM('')
);
#126=(
BOUNDED_CURVE()
B_SPLINE_CURVE(2,(#3142,#3143,#3144),.UNSPECIFIED.,.F.,.F.)
B_SPLINE_CURVE_WITH_KNOTS((3,3),(0.868406111432417,1.41937598717135),
 .UNSPECIFIED.)
CURVE()
GEOMETRIC_REPRESENTATION_ITEM()
RATIONAL_B_SPLINE_CURVE((1.77300220810192,1.91014440617348,1.91014440617348))
REPRESENTATION_ITEM('')
);
#127=(
BOUNDED_CURVE()
B_SPLINE_CURVE(2,(#3145,#3146,#3147),.UNSPECIFIED.,.F.,.F.)
B_SPLINE_CURVE_WITH_KNOTS((3,3),(1.41937598717135,1.97034586291028),
 .UNSPECIFIED.)
CURVE()
GEOMETRIC_REPRESENTATION_ITEM()
RATIONAL_B_SPLINE_CURVE((1.91014440617348,1.91014440617348,1.77300220810192))
REPRESENTATION_ITEM('')
);
#128=(
BOUNDED_CURVE()
B_SPLINE_CURVE(2,(#3169,#3170,#3171),.UNSPECIFIED.,.F.,.F.)
B_SPLINE_CURVE_WITH_KNOTS((3,3),(-1.41937608879025,-0.868406186943507),
 .UNSPECIFIED.)
CURVE()
GEOMETRIC_REPRESENTATION_ITEM()
RATIONAL_B_SPLINE_CURVE((1.91014449034812,1.91014449034812,1.7730022862331))
REPRESENTATION_ITEM('')
);
#129=(
BOUNDED_CURVE()
B_SPLINE_CURVE(2,(#3172,#3173,#3174),.UNSPECIFIED.,.F.,.F.)
B_SPLINE_CURVE_WITH_KNOTS((3,3),(-1.97034599063699,-1.41937608879025),
 .UNSPECIFIED.)
CURVE()
GEOMETRIC_REPRESENTATION_ITEM()
RATIONAL_B_SPLINE_CURVE((1.7730022862331,1.91014449034812,1.91014449034812))
REPRESENTATION_ITEM('')
);
#130=(
BOUNDED_CURVE()
B_SPLINE_CURVE(2,(#3196,#3197,#3198),.UNSPECIFIED.,.F.,.F.)
B_SPLINE_CURVE_WITH_KNOTS((3,3),(0.868406111432395,1.41937598717132),
 .UNSPECIFIED.)
CURVE()
GEOMETRIC_REPRESENTATION_ITEM()
RATIONAL_B_SPLINE_CURVE((1.7730022081019,1.91014440617345,1.91014440617345))
REPRESENTATION_ITEM('')
);
#131=(
BOUNDED_CURVE()
B_SPLINE_CURVE(2,(#3199,#3200,#3201),.UNSPECIFIED.,.F.,.F.)
B_SPLINE_CURVE_WITH_KNOTS((3,3),(1.41937598717132,1.97034586291024),
 .UNSPECIFIED.)
CURVE()
GEOMETRIC_REPRESENTATION_ITEM()
RATIONAL_B_SPLINE_CURVE((1.91014440617345,1.91014440617345,1.7730022081019))
REPRESENTATION_ITEM('')
);
#132=(
BOUNDED_CURVE()
B_SPLINE_CURVE(2,(#3220,#3221,#3222),.UNSPECIFIED.,.F.,.F.)
B_SPLINE_CURVE_WITH_KNOTS((3,3),(0.868406111432386,1.41937598717131),
 .UNSPECIFIED.)
CURVE()
GEOMETRIC_REPRESENTATION_ITEM()
RATIONAL_B_SPLINE_CURVE((1.77300220810189,1.91014440617345,1.91014440617345))
REPRESENTATION_ITEM('')
);
#133=(
BOUNDED_CURVE()
B_SPLINE_CURVE(2,(#3223,#3224,#3225),.UNSPECIFIED.,.F.,.F.)
B_SPLINE_CURVE_WITH_KNOTS((3,3),(1.41937598717131,1.97034586291023),
 .UNSPECIFIED.)
CURVE()
GEOMETRIC_REPRESENTATION_ITEM()
RATIONAL_B_SPLINE_CURVE((1.91014440617345,1.91014440617345,1.77300220810189))
REPRESENTATION_ITEM('')
);
#152=B_SPLINE_CURVE_WITH_KNOTS('',3,(#3069,#3070,#3071,#3072,#3073,#3074,
#3075,#3076,#3077,#3078,#3079,#3080,#3081,#3082,#3083,#3084),
 .UNSPECIFIED.,.F.,.F.,(4,3,3,3,3,4),(0.,0.00144938529899606,0.00287700433635734,
0.00289877059799213,0.00434815589698819,0.00579754119598426),
 .UNSPECIFIED.);
#153=B_SPLINE_CURVE_WITH_KNOTS('',3,(#3096,#3097,#3098,#3099,#3100,#3101,
#3102,#3103,#3104,#3105,#3106,#3107,#3108,#3109,#3110,#3111),
 .UNSPECIFIED.,.F.,.F.,(4,3,3,3,3,4),(0.,0.0014493633079017,0.00287680164649716,
0.0028987266158034,0.0043480899237051,0.0057974532316068),.UNSPECIFIED.);
#154=B_SPLINE_CURVE_WITH_KNOTS('',3,(#3123,#3124,#3125,#3126,#3127,#3128,
#3129,#3130,#3131,#3132,#3133,#3134,#3135,#3136,#3137,#3138),
 .UNSPECIFIED.,.F.,.F.,(4,3,3,3,3,4),(1.17946057326806E-18,0.0014493633079017,
0.00287680164649714,0.0028987266158034,0.0043480899237051,0.0057974532316068),
 .UNSPECIFIED.);
#155=B_SPLINE_CURVE_WITH_KNOTS('',3,(#3150,#3151,#3152,#3153,#3154,#3155,
#3156,#3157,#3158,#3159,#3160,#3161,#3162,#3163,#3164,#3165),
 .UNSPECIFIED.,.F.,.F.,(4,3,3,3,3,4),(0.,0.00144934135226602,0.00287664328376737,
0.00289868270453203,0.00434802405679805,0.00579736540906406),
 .UNSPECIFIED.);
#156=B_SPLINE_CURVE_WITH_KNOTS('',3,(#3177,#3178,#3179,#3180,#3181,#3182,
#3183,#3184,#3185,#3186,#3187,#3188,#3189,#3190,#3191,#3192),
 .UNSPECIFIED.,.F.,.F.,(4,3,3,3,3,4),(0.,0.0014493633079017,0.00287680164649716,
0.0028987266158034,0.0043480899237051,0.0057974532316068),.UNSPECIFIED.);
#157=B_SPLINE_CURVE_WITH_KNOTS('',3,(#3203,#3204,#3205,#3206,#3207,#3208,
#3209,#3210,#3211,#3212,#3213,#3214,#3215,#3216,#3217,#3218),
 .UNSPECIFIED.,.F.,.F.,(4,3,3,3,3,4),(3.71652746642586E-20,0.0014493633079017,
0.00287680164649716,0.0028987266158034,0.0043480899237051,0.0057974532316068),
 .UNSPECIFIED.);
#158=B_SPLINE_CURVE_WITH_KNOTS('',3,(#3261,#3262,#3263,#3264,#3265),
 .UNSPECIFIED.,.F.,.F.,(4,1,4),(0.,0.00306035141916462,0.00612069810971412),
 .UNSPECIFIED.);
#159=B_SPLINE_CURVE_WITH_KNOTS('',3,(#3267,#3268,#3269,#3270,#3271),
 .UNSPECIFIED.,.F.,.F.,(4,1,4),(0.,0.00306038411039262,0.00612076331150472),
 .UNSPECIFIED.);
#160=B_SPLINE_CURVE_WITH_KNOTS('',3,(#3273,#3274,#3275,#3276,#3277),
 .UNSPECIFIED.,.F.,.F.,(4,1,4),(0.,0.00306035141916462,0.00612069797754228),
 .UNSPECIFIED.);
#161=B_SPLINE_CURVE_WITH_KNOTS('',3,(#3279,#3280,#3281,#3282,#3283),
 .UNSPECIFIED.,.F.,.F.,(4,1,4),(0.,0.00306035141916462,0.0061206980316515),
 .UNSPECIFIED.);
#162=B_SPLINE_CURVE_WITH_KNOTS('',3,(#3285,#3286,#3287,#3288,#3289),
 .UNSPECIFIED.,.F.,.F.,(4,1,4),(0.,0.00306031874524394,0.00612063285858316),
 .UNSPECIFIED.);
#163=B_SPLINE_CURVE_WITH_KNOTS('',3,(#3290,#3291,#3292,#3293,#3294),
 .UNSPECIFIED.,.F.,.F.,(4,1,4),(0.,0.00306035141916462,0.0061206982998644),
 .UNSPECIFIED.);
#164=B_SPLINE_CURVE_WITH_KNOTS('',3,(#3313,#3314,#3315,#3316,#3317,#3318,
#3319,#3320,#3321,#3322,#3323,#3324),.UNSPECIFIED.,.F.,.F.,(4,2,2,2,2,4),
(0.,0.0128141897701953,0.02694790056044,0.0403327677820611,0.0535291831368547,
0.0561361462772446),.UNSPECIFIED.);
#165=B_SPLINE_CURVE_WITH_KNOTS('',3,(#3325,#3326,#3327,#3328,#3329,#3330,
#3331,#3332,#3333,#3334,#3335,#3336),.UNSPECIFIED.,.F.,.F.,(4,2,2,2,2,4),
(-0.0537148048665765,-0.0408567535476394,-0.0266745253232854,-0.0132433858241141,
0.,0.00261137592542538),.UNSPECIFIED.);
#166=B_SPLINE_CURVE_WITH_KNOTS('',3,(#3352,#3353,#3354,#3355,#3356,#3357,
#3358,#3359,#3360,#3361,#3362,#3363),.UNSPECIFIED.,.F.,.F.,(4,2,2,2,2,4),
(-0.0537150980019462,-0.040856939694021,-0.0266745961838983,-0.0132434100107398,
0.,0.00261147527362479),.UNSPECIFIED.);
#167=B_SPLINE_CURVE_WITH_KNOTS('',3,(#3379,#3380,#3381,#3382,#3383,#3384,
#3385,#3386,#3387,#3388,#3389,#3390),.UNSPECIFIED.,.F.,.F.,(4,2,2,2,2,4),
(0.,0.0128141921500334,0.0269478992409766,0.0403327871050577,0.0535292168707035,
0.0561361567166107),.UNSPECIFIED.);
#168=B_SPLINE_CURVE_WITH_KNOTS('',3,(#3406,#3407,#3408,#3409,#3410,#3411,
#3412,#3413,#3414,#3415,#3416,#3417),.UNSPECIFIED.,.F.,.F.,(4,2,2,2,2,4),
(-0.0537154001549951,-0.0408571973817338,-0.0266748056367786,-0.013243506422928,
0.,0.00261149488798623),.UNSPECIFIED.);
#169=B_SPLINE_CURVE_WITH_KNOTS('',3,(#3433,#3434,#3435,#3436,#3437,#3438,
#3439,#3440,#3441,#3442,#3443,#3444),.UNSPECIFIED.,.F.,.F.,(4,2,2,2,2,4),
(0.,0.0128142026815068,0.0269479237273733,0.0403328127900412,0.0535292370600361,
0.0561362028969855),.UNSPECIFIED.);
#190=SHAPE_REPRESENTATION_RELATIONSHIP('SRR','None',#3867,#196);
#196=ADVANCED_BREP_SHAPE_REPRESENTATION('',(#208),#3830);
#202=STYLED_ITEM('',(#3905),#208);
#208=MANIFOLD_SOLID_BREP('Body1',#1787);
#225=FACE_BOUND('',#454,.T.);
#226=FACE_BOUND('',#457,.T.);
#252=PLANE('',#1952);
#253=PLANE('',#1953);
#254=PLANE('',#1954);
#255=PLANE('',#1955);
#256=PLANE('',#1956);
#257=PLANE('',#1957);
#258=PLANE('',#1958);
#259=PLANE('',#1970);
#328=FACE_OUTER_BOUND('',#447,.T.);
#329=FACE_OUTER_BOUND('',#448,.T.);
#330=FACE_OUTER_BOUND('',#449,.T.);
#331=FACE_OUTER_BOUND('',#450,.T.);
#332=FACE_OUTER_BOUND('',#451,.T.);
#333=FACE_OUTER_BOUND('',#452,.T.);
#334=FACE_OUTER_BOUND('',#453,.T.);
#335=FACE_OUTER_BOUND('',#455,.T.);
#336=FACE_OUTER_BOUND('',#456,.T.);
#337=FACE_OUTER_BOUND('',#458,.T.);
#338=FACE_OUTER_BOUND('',#459,.T.);
#339=FACE_OUTER_BOUND('',#460,.T.);
#340=FACE_OUTER_BOUND('',#461,.T.);
#341=FACE_OUTER_BOUND('',#462,.T.);
#342=FACE_OUTER_BOUND('',#463,.T.);
#343=FACE_OUTER_BOUND('',#464,.T.);
#344=FACE_OUTER_BOUND('',#465,.T.);
#345=FACE_OUTER_BOUND('',#466,.T.);
#346=FACE_OUTER_BOUND('',#467,.T.);
#347=FACE_OUTER_BOUND('',#468,.T.);
#348=FACE_OUTER_BOUND('',#469,.T.);
#349=FACE_OUTER_BOUND('',#470,.T.);
#350=FACE_OUTER_BOUND('',#471,.T.);
#351=FACE_OUTER_BOUND('',#472,.T.);
#352=FACE_OUTER_BOUND('',#473,.T.);
#447=EDGE_LOOP('',(#1387,#1388,#1389,#1390,#1391));
#448=EDGE_LOOP('',(#1392,#1393,#1394,#1395,#1396));
#449=EDGE_LOOP('',(#1397,#1398,#1399,#1400,#1401));
#450=EDGE_LOOP('',(#1402,#1403,#1404,#1405,#1406));
#451=EDGE_LOOP('',(#1407,#1408,#1409,#1410,#1411));
#452=EDGE_LOOP('',(#1412,#1413,#1414,#1415,#1416));
#453=EDGE_LOOP('',(#1417,#1418,#1419,#1420,#1421,#1422));
#454=EDGE_LOOP('',(#1423));
#455=EDGE_LOOP('',(#1424,#1425,#1426,#1427,#1428));
#456=EDGE_LOOP('',(#1429));
#457=EDGE_LOOP('',(#1430));
#458=EDGE_LOOP('',(#1431,#1432,#1433));
#459=EDGE_LOOP('',(#1434,#1435,#1436));
#460=EDGE_LOOP('',(#1437,#1438,#1439));
#461=EDGE_LOOP('',(#1440,#1441,#1442));
#462=EDGE_LOOP('',(#1443,#1444,#1445));
#463=EDGE_LOOP('',(#1446,#1447,#1448));
#464=EDGE_LOOP('',(#1449,#1450,#1451,#1452,#1453,#1454,#1455,#1456,#1457,
#1458));
#465=EDGE_LOOP('',(#1459,#1460,#1461,#1462,#1463));
#466=EDGE_LOOP('',(#1464,#1465,#1466,#1467));
#467=EDGE_LOOP('',(#1468,#1469,#1470,#1471));
#468=EDGE_LOOP('',(#1472,#1473,#1474,#1475));
#469=EDGE_LOOP('',(#1476,#1477,#1478,#1479));
#470=EDGE_LOOP('',(#1480,#1481,#1482,#1483));
#471=EDGE_LOOP('',(#1484,#1485,#1486,#1487));
#472=EDGE_LOOP('',(#1488,#1489,#1490,#1491));
#473=EDGE_LOOP('',(#1492,#1493,#1494,#1495,#1496));
#544=LINE('',#3067,#637);
#545=LINE('',#3086,#638);
#546=LINE('',#3113,#639);
#547=LINE('',#3140,#640);
#548=LINE('',#3167,#641);
#549=LINE('',#3194,#642);
#550=LINE('',#3240,#643);
#551=LINE('',#3259,#644);
#552=LINE('',#3461,#645);
#553=LINE('',#3463,#646);
#637=VECTOR('',#2288,1.);
#638=VECTOR('',#2289,1.);
#639=VECTOR('',#2292,1.);
#640=VECTOR('',#2295,1.);
#641=VECTOR('',#2298,1.);
#642=VECTOR('',#2301,1.);
#643=VECTOR('',#2324,0.0024585);
#644=VECTOR('',#2351,0.00672685951651014);
#645=VECTOR('',#2360,0.003);
#646=VECTOR('',#2363,0.0024585);
#725=CIRCLE('',#1959,0.005);
#726=CIRCLE('',#1960,0.005);
#727=CIRCLE('',#1961,0.005);
#728=CIRCLE('',#1962,0.005);
#729=CIRCLE('',#1963,0.005);
#730=CIRCLE('',#1964,0.005);
#731=CIRCLE('',#1965,0.003);
#732=CIRCLE('',#1967,0.0024585);
#733=CIRCLE('',#1968,0.0024585);
#734=CIRCLE('',#1969,0.0024585);
#735=CIRCLE('',#1971,0.00653289983773083);
#736=CIRCLE('',#1972,0.003);
#737=CIRCLE('',#1980,0.00672685951651014);
#738=CIRCLE('',#1981,0.00672685951651014);
#739=CIRCLE('',#1983,0.000567100162269171);
#819=VERTEX_POINT('',#3065);
#820=VERTEX_POINT('',#3066);
#821=VERTEX_POINT('',#3068);
#822=VERTEX_POINT('',#3085);
#823=VERTEX_POINT('',#3087);
#824=VERTEX_POINT('',#3095);
#825=VERTEX_POINT('',#3112);
#826=VERTEX_POINT('',#3114);
#827=VERTEX_POINT('',#3122);
#828=VERTEX_POINT('',#3139);
#829=VERTEX_POINT('',#3141);
#830=VERTEX_POINT('',#3149);
#831=VERTEX_POINT('',#3166);
#832=VERTEX_POINT('',#3168);
#833=VERTEX_POINT('',#3176);
#834=VERTEX_POINT('',#3193);
#835=VERTEX_POINT('',#3195);
#836=VERTEX_POINT('',#3219);
#837=VERTEX_POINT('',#3233);
#838=VERTEX_POINT('',#3236);
#839=VERTEX_POINT('',#3237);
#840=VERTEX_POINT('',#3239);
#841=VERTEX_POINT('',#3244);
#842=VERTEX_POINT('',#3246);
#843=VERTEX_POINT('',#3255);
#844=VERTEX_POINT('',#3256);
#845=VERTEX_POINT('',#3258);
#846=VERTEX_POINT('',#3260);
#847=VERTEX_POINT('',#3266);
#848=VERTEX_POINT('',#3272);
#849=VERTEX_POINT('',#3278);
#850=VERTEX_POINT('',#3284);
#1020=EDGE_CURVE('',#819,#820,#544,.T.);
#1021=EDGE_CURVE('',#820,#821,#152,.T.);
#1022=EDGE_CURVE('',#822,#821,#545,.T.);
#1023=EDGE_CURVE('',#822,#823,#122,.T.);
#1024=EDGE_CURVE('',#823,#819,#123,.T.);
#1025=EDGE_CURVE('',#821,#824,#153,.T.);
#1026=EDGE_CURVE('',#825,#824,#546,.T.);
#1027=EDGE_CURVE('',#825,#826,#124,.T.);
#1028=EDGE_CURVE('',#826,#822,#125,.T.);
#1029=EDGE_CURVE('',#824,#827,#154,.T.);
#1030=EDGE_CURVE('',#828,#827,#547,.T.);
#1031=EDGE_CURVE('',#828,#829,#126,.T.);
#1032=EDGE_CURVE('',#829,#825,#127,.T.);
#1033=EDGE_CURVE('',#827,#830,#155,.T.);
#1034=EDGE_CURVE('',#831,#830,#548,.T.);
#1035=EDGE_CURVE('',#831,#832,#128,.F.);
#1036=EDGE_CURVE('',#832,#828,#129,.F.);
#1037=EDGE_CURVE('',#830,#833,#156,.T.);
#1038=EDGE_CURVE('',#834,#833,#549,.T.);
#1039=EDGE_CURVE('',#834,#835,#130,.T.);
#1040=EDGE_CURVE('',#835,#831,#131,.T.);
#1041=EDGE_CURVE('',#833,#820,#157,.T.);
#1042=EDGE_CURVE('',#819,#836,#132,.T.);
#1043=EDGE_CURVE('',#836,#834,#133,.T.);
#1044=EDGE_CURVE('',#835,#836,#725,.T.);
#1045=EDGE_CURVE('',#836,#823,#726,.T.);
#1046=EDGE_CURVE('',#823,#826,#727,.T.);
#1047=EDGE_CURVE('',#826,#829,#728,.T.);
#1048=EDGE_CURVE('',#829,#832,#729,.T.);
#1049=EDGE_CURVE('',#832,#835,#730,.T.);
#1050=EDGE_CURVE('',#837,#837,#731,.F.);
#1051=EDGE_CURVE('',#838,#839,#732,.T.);
#1052=EDGE_CURVE('',#839,#840,#550,.T.);
#1053=EDGE_CURVE('',#840,#840,#733,.F.);
#1054=EDGE_CURVE('',#839,#838,#734,.T.);
#1055=EDGE_CURVE('',#841,#841,#735,.T.);
#1056=EDGE_CURVE('',#842,#842,#736,.T.);
#1057=EDGE_CURVE('',#843,#844,#737,.T.);
#1058=EDGE_CURVE('',#844,#845,#551,.T.);
#1059=EDGE_CURVE('',#845,#846,#158,.T.);
#1060=EDGE_CURVE('',#846,#847,#159,.T.);
#1061=EDGE_CURVE('',#847,#848,#160,.T.);
#1062=EDGE_CURVE('',#848,#849,#161,.T.);
#1063=EDGE_CURVE('',#849,#850,#162,.T.);
#1064=EDGE_CURVE('',#850,#845,#163,.T.);
#1065=EDGE_CURVE('',#844,#843,#738,.T.);
#1066=EDGE_CURVE('',#843,#841,#739,.T.);
#1067=EDGE_CURVE('',#847,#827,#164,.F.);
#1068=EDGE_CURVE('',#830,#846,#165,.T.);
#1069=EDGE_CURVE('',#833,#845,#166,.T.);
#1070=EDGE_CURVE('',#848,#824,#167,.F.);
#1071=EDGE_CURVE('',#820,#850,#168,.T.);
#1072=EDGE_CURVE('',#849,#821,#169,.F.);
#1073=EDGE_CURVE('',#840,#842,#552,.T.);
#1074=EDGE_CURVE('',#838,#837,#553,.T.);
#1387=ORIENTED_EDGE('',*,*,#1020,.T.);
#1388=ORIENTED_EDGE('',*,*,#1021,.T.);
#1389=ORIENTED_EDGE('',*,*,#1022,.F.);
#1390=ORIENTED_EDGE('',*,*,#1023,.T.);
#1391=ORIENTED_EDGE('',*,*,#1024,.T.);
#1392=ORIENTED_EDGE('',*,*,#1022,.T.);
#1393=ORIENTED_EDGE('',*,*,#1025,.T.);
#1394=ORIENTED_EDGE('',*,*,#1026,.F.);
#1395=ORIENTED_EDGE('',*,*,#1027,.T.);
#1396=ORIENTED_EDGE('',*,*,#1028,.T.);
#1397=ORIENTED_EDGE('',*,*,#1026,.T.);
#1398=ORIENTED_EDGE('',*,*,#1029,.T.);
#1399=ORIENTED_EDGE('',*,*,#1030,.F.);
#1400=ORIENTED_EDGE('',*,*,#1031,.T.);
#1401=ORIENTED_EDGE('',*,*,#1032,.T.);
#1402=ORIENTED_EDGE('',*,*,#1030,.T.);
#1403=ORIENTED_EDGE('',*,*,#1033,.T.);
#1404=ORIENTED_EDGE('',*,*,#1034,.F.);
#1405=ORIENTED_EDGE('',*,*,#1035,.T.);
#1406=ORIENTED_EDGE('',*,*,#1036,.T.);
#1407=ORIENTED_EDGE('',*,*,#1034,.T.);
#1408=ORIENTED_EDGE('',*,*,#1037,.T.);
#1409=ORIENTED_EDGE('',*,*,#1038,.F.);
#1410=ORIENTED_EDGE('',*,*,#1039,.T.);
#1411=ORIENTED_EDGE('',*,*,#1040,.T.);
#1412=ORIENTED_EDGE('',*,*,#1038,.T.);
#1413=ORIENTED_EDGE('',*,*,#1041,.T.);
#1414=ORIENTED_EDGE('',*,*,#1020,.F.);
#1415=ORIENTED_EDGE('',*,*,#1042,.T.);
#1416=ORIENTED_EDGE('',*,*,#1043,.T.);
#1417=ORIENTED_EDGE('',*,*,#1044,.T.);
#1418=ORIENTED_EDGE('',*,*,#1045,.T.);
#1419=ORIENTED_EDGE('',*,*,#1046,.T.);
#1420=ORIENTED_EDGE('',*,*,#1047,.T.);
#1421=ORIENTED_EDGE('',*,*,#1048,.T.);
#1422=ORIENTED_EDGE('',*,*,#1049,.T.);
#1423=ORIENTED_EDGE('',*,*,#1050,.T.);
#1424=ORIENTED_EDGE('',*,*,#1051,.T.);
#1425=ORIENTED_EDGE('',*,*,#1052,.T.);
#1426=ORIENTED_EDGE('',*,*,#1053,.T.);
#1427=ORIENTED_EDGE('',*,*,#1052,.F.);
#1428=ORIENTED_EDGE('',*,*,#1054,.T.);
#1429=ORIENTED_EDGE('',*,*,#1055,.F.);
#1430=ORIENTED_EDGE('',*,*,#1056,.T.);
#1431=ORIENTED_EDGE('',*,*,#1043,.F.);
#1432=ORIENTED_EDGE('',*,*,#1044,.F.);
#1433=ORIENTED_EDGE('',*,*,#1039,.F.);
#1434=ORIENTED_EDGE('',*,*,#1045,.F.);
#1435=ORIENTED_EDGE('',*,*,#1042,.F.);
#1436=ORIENTED_EDGE('',*,*,#1024,.F.);
#1437=ORIENTED_EDGE('',*,*,#1040,.F.);
#1438=ORIENTED_EDGE('',*,*,#1049,.F.);
#1439=ORIENTED_EDGE('',*,*,#1035,.F.);
#1440=ORIENTED_EDGE('',*,*,#1036,.F.);
#1441=ORIENTED_EDGE('',*,*,#1048,.F.);
#1442=ORIENTED_EDGE('',*,*,#1031,.F.);
#1443=ORIENTED_EDGE('',*,*,#1047,.F.);
#1444=ORIENTED_EDGE('',*,*,#1027,.F.);
#1445=ORIENTED_EDGE('',*,*,#1032,.F.);
#1446=ORIENTED_EDGE('',*,*,#1046,.F.);
#1447=ORIENTED_EDGE('',*,*,#1023,.F.);
#1448=ORIENTED_EDGE('',*,*,#1028,.F.);
#1449=ORIENTED_EDGE('',*,*,#1057,.T.);
#1450=ORIENTED_EDGE('',*,*,#1058,.T.);
#1451=ORIENTED_EDGE('',*,*,#1059,.T.);
#1452=ORIENTED_EDGE('',*,*,#1060,.T.);
#1453=ORIENTED_EDGE('',*,*,#1061,.T.);
#1454=ORIENTED_EDGE('',*,*,#1062,.T.);
#1455=ORIENTED_EDGE('',*,*,#1063,.T.);
#1456=ORIENTED_EDGE('',*,*,#1064,.T.);
#1457=ORIENTED_EDGE('',*,*,#1058,.F.);
#1458=ORIENTED_EDGE('',*,*,#1065,.T.);
#1459=ORIENTED_EDGE('',*,*,#1057,.F.);
#1460=ORIENTED_EDGE('',*,*,#1066,.T.);
#1461=ORIENTED_EDGE('',*,*,#1055,.T.);
#1462=ORIENTED_EDGE('',*,*,#1066,.F.);
#1463=ORIENTED_EDGE('',*,*,#1065,.F.);
#1464=ORIENTED_EDGE('',*,*,#1067,.F.);
#1465=ORIENTED_EDGE('',*,*,#1060,.F.);
#1466=ORIENTED_EDGE('',*,*,#1068,.F.);
#1467=ORIENTED_EDGE('',*,*,#1033,.F.);
#1468=ORIENTED_EDGE('',*,*,#1068,.T.);
#1469=ORIENTED_EDGE('',*,*,#1059,.F.);
#1470=ORIENTED_EDGE('',*,*,#1069,.F.);
#1471=ORIENTED_EDGE('',*,*,#1037,.F.);
#1472=ORIENTED_EDGE('',*,*,#1067,.T.);
#1473=ORIENTED_EDGE('',*,*,#1029,.F.);
#1474=ORIENTED_EDGE('',*,*,#1070,.F.);
#1475=ORIENTED_EDGE('',*,*,#1061,.F.);
#1476=ORIENTED_EDGE('',*,*,#1069,.T.);
#1477=ORIENTED_EDGE('',*,*,#1064,.F.);
#1478=ORIENTED_EDGE('',*,*,#1071,.F.);
#1479=ORIENTED_EDGE('',*,*,#1041,.F.);
#1480=ORIENTED_EDGE('',*,*,#1070,.T.);
#1481=ORIENTED_EDGE('',*,*,#1025,.F.);
#1482=ORIENTED_EDGE('',*,*,#1072,.F.);
#1483=ORIENTED_EDGE('',*,*,#1062,.F.);
#1484=ORIENTED_EDGE('',*,*,#1071,.T.);
#1485=ORIENTED_EDGE('',*,*,#1063,.F.);
#1486=ORIENTED_EDGE('',*,*,#1072,.T.);
#1487=ORIENTED_EDGE('',*,*,#1021,.F.);
#1488=ORIENTED_EDGE('',*,*,#1053,.F.);
#1489=ORIENTED_EDGE('',*,*,#1073,.T.);
#1490=ORIENTED_EDGE('',*,*,#1056,.F.);
#1491=ORIENTED_EDGE('',*,*,#1073,.F.);
#1492=ORIENTED_EDGE('',*,*,#1051,.F.);
#1493=ORIENTED_EDGE('',*,*,#1074,.T.);
#1494=ORIENTED_EDGE('',*,*,#1050,.F.);
#1495=ORIENTED_EDGE('',*,*,#1074,.F.);
#1496=ORIENTED_EDGE('',*,*,#1054,.F.);
#1667=CYLINDRICAL_SURFACE('',#1966,0.0024585);
#1734=ADVANCED_FACE('',(#328),#252,.T.);
#1735=ADVANCED_FACE('',(#329),#253,.T.);
#1736=ADVANCED_FACE('',(#330),#254,.T.);
#1737=ADVANCED_FACE('',(#331),#255,.T.);
#1738=ADVANCED_FACE('',(#332),#256,.T.);
#1739=ADVANCED_FACE('',(#333),#257,.T.);
#1740=ADVANCED_FACE('',(#334,#225),#258,.T.);
#1741=ADVANCED_FACE('',(#335),#1667,.F.);
#1742=ADVANCED_FACE('',(#336,#226),#259,.F.);
#1743=ADVANCED_FACE('',(#337),#101,.T.);
#1744=ADVANCED_FACE('',(#338),#102,.T.);
#1745=ADVANCED_FACE('',(#339),#103,.T.);
#1746=ADVANCED_FACE('',(#340),#104,.T.);
#1747=ADVANCED_FACE('',(#341),#105,.T.);
#1748=ADVANCED_FACE('',(#342),#106,.T.);
#1749=ADVANCED_FACE('',(#343),#107,.T.);
#1750=ADVANCED_FACE('',(#344),#92,.T.);
#1751=ADVANCED_FACE('',(#345),#84,.F.);
#1752=ADVANCED_FACE('',(#346),#85,.F.);
#1753=ADVANCED_FACE('',(#347),#86,.F.);
#1754=ADVANCED_FACE('',(#348),#87,.F.);
#1755=ADVANCED_FACE('',(#349),#88,.F.);
#1756=ADVANCED_FACE('',(#350),#89,.F.);
#1757=ADVANCED_FACE('',(#351),#108,.F.);
#1758=ADVANCED_FACE('',(#352),#109,.F.);
#1787=CLOSED_SHELL('',(#1734,#1735,#1736,#1737,#1738,#1739,#1740,#1741,
#1742,#1743,#1744,#1745,#1746,#1747,#1748,#1749,#1750,#1751,#1752,#1753,
#1754,#1755,#1756,#1757,#1758));
#1951=AXIS2_PLACEMENT_3D('',#3063,#2284,#2285);
#1952=AXIS2_PLACEMENT_3D('',#3064,#2286,#2287);
#1953=AXIS2_PLACEMENT_3D('',#3094,#2290,#2291);
#1954=AXIS2_PLACEMENT_3D('',#3121,#2293,#2294);
#1955=AXIS2_PLACEMENT_3D('',#3148,#2296,#2297);
#1956=AXIS2_PLACEMENT_3D('',#3175,#2299,#2300);
#1957=AXIS2_PLACEMENT_3D('',#3202,#2302,#2303);
#1958=AXIS2_PLACEMENT_3D('',#3226,#2304,#2305);
#1959=AXIS2_PLACEMENT_3D('',#3227,#2306,#2307);
#1960=AXIS2_PLACEMENT_3D('',#3228,#2308,#2309);
#1961=AXIS2_PLACEMENT_3D('',#3229,#2310,#2311);
#1962=AXIS2_PLACEMENT_3D('',#3230,#2312,#2313);
#1963=AXIS2_PLACEMENT_3D('',#3231,#2314,#2315);
#1964=AXIS2_PLACEMENT_3D('',#3232,#2316,#2317);
#1965=AXIS2_PLACEMENT_3D('',#3234,#2318,#2319);
#1966=AXIS2_PLACEMENT_3D('',#3235,#2320,#2321);
#1967=AXIS2_PLACEMENT_3D('',#3238,#2322,#2323);
#1968=AXIS2_PLACEMENT_3D('',#3241,#2325,#2326);
#1969=AXIS2_PLACEMENT_3D('',#3242,#2327,#2328);
#1970=AXIS2_PLACEMENT_3D('',#3243,#2329,#2330);
#1971=AXIS2_PLACEMENT_3D('',#3245,#2331,#2332);
#1972=AXIS2_PLACEMENT_3D('',#3247,#2333,#2334);
#1973=AXIS2_PLACEMENT_3D('',#3248,#2335,#2336);
#1974=AXIS2_PLACEMENT_3D('',#3249,#2337,#2338);
#1975=AXIS2_PLACEMENT_3D('',#3250,#2339,#2340);
#1976=AXIS2_PLACEMENT_3D('',#3251,#2341,#2342);
#1977=AXIS2_PLACEMENT_3D('',#3252,#2343,#2344);
#1978=AXIS2_PLACEMENT_3D('',#3253,#2345,#2346);
#1979=AXIS2_PLACEMENT_3D('',#3254,#2347,#2348);
#1980=AXIS2_PLACEMENT_3D('',#3257,#2349,#2350);
#1981=AXIS2_PLACEMENT_3D('',#3295,#2352,#2353);
#1982=AXIS2_PLACEMENT_3D('',#3296,#2354,#2355);
#1983=AXIS2_PLACEMENT_3D('',#3297,#2356,#2357);
#1984=AXIS2_PLACEMENT_3D('',#3460,#2358,#2359);
#1985=AXIS2_PLACEMENT_3D('',#3462,#2361,#2362);
#2284=DIRECTION('axis',(0.,0.,1.));
#2285=DIRECTION('refdir',(1.,0.,0.));
#2286=DIRECTION('center_axis',(0.,1.,0.));
#2287=DIRECTION('ref_axis',(0.,0.,1.));
#2288=DIRECTION('',(0.,0.,-1.));
#2289=DIRECTION('',(0.,0.,-1.));
#2290=DIRECTION('center_axis',(-0.866025403784438,0.5,0.));
#2291=DIRECTION('ref_axis',(-0.5,-0.866025403784438,0.));
#2292=DIRECTION('',(0.,0.,-1.));
#2293=DIRECTION('center_axis',(-0.866025403784438,-0.5,0.));
#2294=DIRECTION('ref_axis',(0.5,-0.866025403784438,0.));
#2295=DIRECTION('',(0.,0.,-1.));
#2296=DIRECTION('center_axis',(0.,-1.,0.));
#2297=DIRECTION('ref_axis',(0.,0.,-1.));
#2298=DIRECTION('',(0.,0.,-1.));
#2299=DIRECTION('center_axis',(0.866025403784439,-0.5,0.));
#2300=DIRECTION('ref_axis',(0.5,0.866025403784439,0.));
#2301=DIRECTION('',(0.,0.,-1.));
#2302=DIRECTION('center_axis',(0.866025403784438,0.5,0.));
#2303=DIRECTION('ref_axis',(-0.5,0.866025403784438,0.));
#2304=DIRECTION('center_axis',(0.,0.,1.));
#2305=DIRECTION('ref_axis',(1.,0.,0.));
#2306=DIRECTION('center_axis',(0.,0.,1.));
#2307=DIRECTION('ref_axis',(1.,0.,0.));
#2308=DIRECTION('center_axis',(0.,0.,1.));
#2309=DIRECTION('ref_axis',(1.,0.,0.));
#2310=DIRECTION('center_axis',(0.,0.,1.));
#2311=DIRECTION('ref_axis',(1.,0.,0.));
#2312=DIRECTION('center_axis',(0.,0.,1.));
#2313=DIRECTION('ref_axis',(1.,0.,0.));
#2314=DIRECTION('center_axis',(0.,0.,1.));
#2315=DIRECTION('ref_axis',(1.,0.,0.));
#2316=DIRECTION('center_axis',(0.,0.,1.));
#2317=DIRECTION('ref_axis',(1.,0.,0.));
#2318=DIRECTION('center_axis',(0.,0.,1.));
#2319=DIRECTION('ref_axis',(1.,0.,0.));
#2320=DIRECTION('center_axis',(0.,0.,-1.));
#2321=DIRECTION('ref_axis',(-1.,0.,0.));
#2322=DIRECTION('center_axis',(0.,0.,1.));
#2323=DIRECTION('ref_axis',(1.,0.,0.));
#2324=DIRECTION('',(0.,0.,-1.));
#2325=DIRECTION('center_axis',(0.,0.,1.));
#2326=DIRECTION('ref_axis',(1.,0.,0.));
#2327=DIRECTION('center_axis',(0.,0.,1.));
#2328=DIRECTION('ref_axis',(1.,0.,0.));
#2329=DIRECTION('center_axis',(0.,0.,1.));
#2330=DIRECTION('ref_axis',(1.,0.,0.));
#2331=DIRECTION('center_axis',(0.,0.,1.));
#2332=DIRECTION('ref_axis',(1.,0.,0.));
#2333=DIRECTION('center_axis',(0.,0.,1.));
#2334=DIRECTION('ref_axis',(1.,0.,0.));
#2335=DIRECTION('center_axis',(0.,0.,-1.));
#2336=DIRECTION('ref_axis',(1.,5.66553889764798E-16,0.));
#2337=DIRECTION('center_axis',(0.,0.,-1.));
#2338=DIRECTION('ref_axis',(-1.,0.,0.));
#2339=DIRECTION('center_axis',(0.,0.,-1.));
#2340=DIRECTION('ref_axis',(-1.,0.,0.));
#2341=DIRECTION('center_axis',(0.,0.,-1.));
#2342=DIRECTION('ref_axis',(-1.,0.,0.));
#2343=DIRECTION('center_axis',(0.,0.,-1.));
#2344=DIRECTION('ref_axis',(-1.,0.,0.));
#2345=DIRECTION('center_axis',(0.,0.,-1.));
#2346=DIRECTION('ref_axis',(-1.,0.,0.));
#2347=DIRECTION('center_axis',(0.,0.,-1.));
#2348=DIRECTION('ref_axis',(-1.,0.,0.));
#2349=DIRECTION('center_axis',(0.,0.,1.));
#2350=DIRECTION('ref_axis',(1.,0.,0.));
#2351=DIRECTION('',(-0.939692620785908,1.15079156022785E-16,0.342020143325669));
#2352=DIRECTION('center_axis',(0.,0.,1.));
#2353=DIRECTION('ref_axis',(1.,0.,0.));
#2354=DIRECTION('center_axis',(0.,0.,1.));
#2355=DIRECTION('ref_axis',(1.,0.,0.));
#2356=DIRECTION('center_axis',(1.22464679914735E-16,-1.,0.));
#2357=DIRECTION('ref_axis',(-1.,-1.22464679914735E-16,0.));
#2358=DIRECTION('center_axis',(0.,0.,-1.));
#2359=DIRECTION('ref_axis',(-1.,0.,0.));
#2360=DIRECTION('',(0.707106781186547,-8.65956056235493E-17,-0.707106781186548));
#2361=DIRECTION('center_axis',(0.,0.,1.));
#2362=DIRECTION('ref_axis',(1.,0.,0.));
#2363=DIRECTION('',(-0.707106781186547,-8.65956056235493E-17,0.707106781186548));
#3063=CARTESIAN_POINT('',(0.,0.,0.));
#3064=CARTESIAN_POINT('Origin',(0.,0.005,0.003));
#3065=CARTESIAN_POINT('',(0.00288675134594812,0.005,0.0025534180126148));
#3066=CARTESIAN_POINT('',(0.00288675134594812,0.005,-0.00125469561686031));
#3067=CARTESIAN_POINT('',(0.00288675134594812,0.005,0.003));
#3068=CARTESIAN_POINT('',(-0.00288674534909874,0.00499999549622412,-0.0012546876068247));
#3069=CARTESIAN_POINT('Ctrl Pts',(0.00288674086811144,0.005,-0.00125466832470784));
#3070=CARTESIAN_POINT('Ctrl Pts',(0.00240905318327833,0.005,-0.00117291044573697));
#3071=CARTESIAN_POINT('Ctrl Pts',(0.00192881231229982,0.00499999999750974,
-0.00110698869329289));
#3072=CARTESIAN_POINT('Ctrl Pts',(0.00144725210385079,0.00500000000251777,
-0.0010616014875037));
#3073=CARTESIAN_POINT('Ctrl Pts',(0.000972923765006934,0.00500000000745059,
-0.00101689588776968));
#3074=CARTESIAN_POINT('Ctrl Pts',(0.000497315857174576,0.00500000004285957,
-0.00099213963141374));
#3075=CARTESIAN_POINT('Ctrl Pts',(2.17100169132483E-5,0.00500000001549357,
-0.000991518738265624));
#3076=CARTESIAN_POINT('Ctrl Pts',(1.44586698218705E-5,0.00500000001507633,
-0.000991509271788676));
#3077=CARTESIAN_POINT('Ctrl Pts',(7.20731733020144E-6,0.00500000001465332,
-0.000991505417348841));
#3078=CARTESIAN_POINT('Ctrl Pts',(-4.40332323880218E-8,0.00500000001422604,
-0.000991507156144612));
#3079=CARTESIAN_POINT('Ctrl Pts',(-0.000482901451728483,0.00499999998577425,
-0.000991622940153412));
#3080=CARTESIAN_POINT('Ctrl Pts',(-0.000965714799268779,0.005,-0.00101680380767097));
#3081=CARTESIAN_POINT('Ctrl Pts',(-0.00144724102982738,0.005,-0.00106216147680642));
#3082=CARTESIAN_POINT('Ctrl Pts',(-0.00192876726038598,0.005,-0.00110751914594187));
#3083=CARTESIAN_POINT('Ctrl Pts',(-0.00240902863327068,0.005,-0.00117307891969936));
#3084=CARTESIAN_POINT('Ctrl Pts',(-0.00288673415173692,0.005,-0.00125470733476186));
#3085=CARTESIAN_POINT('',(-0.00288675134594812,0.005,0.0025534180126148));
#3086=CARTESIAN_POINT('',(-0.00288675134594813,0.005,0.003));
#3087=CARTESIAN_POINT('',(0.,0.005,0.003));
#3088=CARTESIAN_POINT('Ctrl Pts',(-0.00288675134596021,0.005,0.00255341801261131));
#3089=CARTESIAN_POINT('Ctrl Pts',(-0.00133974596216047,0.005,0.003));
#3090=CARTESIAN_POINT('Ctrl Pts',(0.,0.005,0.003));
#3091=CARTESIAN_POINT('Ctrl Pts',(0.,0.005,0.003));
#3092=CARTESIAN_POINT('Ctrl Pts',(0.00133974596216047,0.005,0.003));
#3093=CARTESIAN_POINT('Ctrl Pts',(0.0028867513459602,0.005,0.00255341801261131));
#3094=CARTESIAN_POINT('Origin',(-0.00433012701892219,0.0025,0.003));
#3095=CARTESIAN_POINT('',(-0.00577349577362417,2.97524700789561E-9,-0.00125468783280795));
#3096=CARTESIAN_POINT('Ctrl Pts',(-0.00288675654646056,0.00499999099244825,
-0.00125466787888755));
#3097=CARTESIAN_POINT('Ctrl Pts',(-0.00312559936895968,0.00458630308885661,
-0.00117290882464078));
#3098=CARTESIAN_POINT('Ctrl Pts',(-0.00336571418606295,0.00417041202041243,
-0.001106984526675));
#3099=CARTESIAN_POINT('Ctrl Pts',(-0.00360648916145778,0.00375337754104142,
-0.00106159956055554));
#3100=CARTESIAN_POINT('Ctrl Pts',(-0.00384362185895275,0.00334265167187877,
-0.0010169011469269));
#3101=CARTESIAN_POINT('Ctrl Pts',(-0.00408139429007746,0.00293081781202513,
-0.000992145259800431));
#3102=CARTESIAN_POINT('Ctrl Pts',(-0.00431917052189825,0.00251897724138379,
-0.000991520603317846));
#3103=CARTESIAN_POINT('Ctrl Pts',(-0.00432282268426734,0.00251265150973835,
-0.000991511008805889));
#3104=CARTESIAN_POINT('Ctrl Pts',(-0.00432647485050128,0.00250632577138726,
-0.000991507108821008));
#3105=CARTESIAN_POINT('Ctrl Pts',(-0.00433012701679626,0.00250000003292203,
-0.00099150888414755));
#3106=CARTESIAN_POINT('Ctrl Pts',(-0.00457155567050904,0.00208183327980953,
-0.000991626243178409));
#3107=CARTESIAN_POINT('Ctrl Pts',(-0.00481296724285258,0.00166369620021464,
-0.00101680902829736));
#3108=CARTESIAN_POINT('Ctrl Pts',(-0.00505373559306525,0.00124667318479177,
-0.00106216623675387));
#3109=CARTESIAN_POINT('Ctrl Pts',(-0.00529450394327791,0.000829650169368897,
-0.00110752344521038));
#3110=CARTESIAN_POINT('Ctrl Pts',(-0.00553464028677118,0.000413721821694746,
-0.00117308056855006));
#3111=CARTESIAN_POINT('Ctrl Pts',(-0.00577349405586451,1.49580457720067E-8,
-0.00125470778672834));
#3112=CARTESIAN_POINT('',(-0.00577350269189626,-1.7347234759768E-18,0.0025534180126148));
#3113=CARTESIAN_POINT('',(-0.00577350269189626,4.33680868994202E-19,0.003));
#3114=CARTESIAN_POINT('',(-0.00433012701892219,0.0025,0.003));
#3115=CARTESIAN_POINT('Ctrl Pts',(-0.0057735026919023,-1.04763274033972E-14,
0.00255341801261131));
#3116=CARTESIAN_POINT('Ctrl Pts',(-0.00500000000000243,0.0013397459621514,
0.003));
#3117=CARTESIAN_POINT('Ctrl Pts',(-0.00433012701892219,0.0025,0.003));
#3118=CARTESIAN_POINT('Ctrl Pts',(-0.00433012701892219,0.0025,0.003));
#3119=CARTESIAN_POINT('Ctrl Pts',(-0.00366025403784195,0.0036602540378486,
0.003));
#3120=CARTESIAN_POINT('Ctrl Pts',(-0.00288675134594208,0.00500000000001047,
0.00255341801261131));
#3121=CARTESIAN_POINT('Origin',(-0.00433012701892219,-0.0025,0.003));
#3122=CARTESIAN_POINT('',(-0.00288675049891667,-0.0049999925209771,-0.00125468762698494));
#3123=CARTESIAN_POINT('Ctrl Pts',(-0.00577349749138383,-9.00755175621548E-9,
-0.00125466787888756));
#3124=CARTESIAN_POINT('Ctrl Pts',(-0.00553465466888472,-0.000413696911143376,
-0.00117290882464071));
#3125=CARTESIAN_POINT('Ctrl Pts',(-0.00529453984695666,-0.000829587976801908,
-0.00110698452667449));
#3126=CARTESIAN_POINT('Ctrl Pts',(-0.00505376488126475,-0.00124662246177494,
-0.00106159956055528));
#3127=CARTESIAN_POINT('Ctrl Pts',(-0.00481663219332592,-0.00165734833645486,
-0.00101690114692689));
#3128=CARTESIAN_POINT('Ctrl Pts',(-0.00457885982411642,-0.00206918223205526,
-0.000992145259800429));
#3129=CARTESIAN_POINT('Ctrl Pts',(-0.00434108354354234,-0.00248102277454885,
-0.000991520603318092));
#3130=CARTESIAN_POINT('Ctrl Pts',(-0.00433743138042441,-0.00248734850576196,
-0.000991511008806138));
#3131=CARTESIAN_POINT('Ctrl Pts',(-0.00433377921343164,-0.00249367424367495,
-0.00099150710882126));
#3132=CARTESIAN_POINT('Ctrl Pts',(-0.00433012704637054,-0.00249999998169787,
-0.000991508884147806));
#3133=CARTESIAN_POINT('Ctrl Pts',(-0.00408869834201345,-0.00291816670557085,
-0.000991626243178921));
#3134=CARTESIAN_POINT('Ctrl Pts',(-0.00384728679499185,-0.00333630379978529,
-0.00101680902829835));
#3135=CARTESIAN_POINT('Ctrl Pts',(-0.00360651844477919,-0.00375332681520815,
-0.00106216623675482));
#3136=CARTESIAN_POINT('Ctrl Pts',(-0.00336575009456654,-0.004170349830631,
-0.00110752344521128));
#3137=CARTESIAN_POINT('Ctrl Pts',(-0.00312561375107325,-0.0045862781783052,
-0.00117308056855045));
#3138=CARTESIAN_POINT('Ctrl Pts',(-0.0028867599819799,-0.00499998504195421,
-0.00125470778672846));
#3139=CARTESIAN_POINT('',(-0.00288675134594813,-0.005,0.0025534180126148));
#3140=CARTESIAN_POINT('',(-0.00288675134594812,-0.005,0.003));
#3141=CARTESIAN_POINT('',(-0.00433012701892219,-0.0025,0.003));
#3142=CARTESIAN_POINT('Ctrl Pts',(-0.00288675134594208,-0.00500000000001047,
0.00255341801261131));
#3143=CARTESIAN_POINT('Ctrl Pts',(-0.00366025403784195,-0.0036602540378486,
0.003));
#3144=CARTESIAN_POINT('Ctrl Pts',(-0.00433012701892219,-0.0025,0.003));
#3145=CARTESIAN_POINT('Ctrl Pts',(-0.00433012701892219,-0.0025,0.003));
#3146=CARTESIAN_POINT('Ctrl Pts',(-0.00500000000000243,-0.0013397459621514,
0.003));
#3147=CARTESIAN_POINT('Ctrl Pts',(-0.0057735026919023,1.04765720059514E-14,
0.00255341801261131));
#3148=CARTESIAN_POINT('Origin',(2.60208521396521E-18,-0.005,0.003));
#3149=CARTESIAN_POINT('',(0.00288674527580217,-0.00499999549622412,-0.00125468803234519));
#3150=CARTESIAN_POINT('Ctrl Pts',(-0.00288674101585344,-0.005,-0.00125466746724142));
#3151=CARTESIAN_POINT('Ctrl Pts',(-0.00240905736903686,-0.005,-0.00117290734672732));
#3152=CARTESIAN_POINT('Ctrl Pts',(-0.00192883892611274,-0.00499999999694111,
-0.0011069808211488));
#3153=CARTESIAN_POINT('Ctrl Pts',(-0.00144729928597653,-0.00500000000309269,
-0.00106159786290637));
#3154=CARTESIAN_POINT('Ctrl Pts',(-0.000973082182196052,-0.00500000000915072,
-0.00101690502097829));
#3155=CARTESIAN_POINT('Ctrl Pts',(-0.000497585721015049,-0.00500000004512902,
-0.000992149362934236));
#3156=CARTESIAN_POINT('Ctrl Pts',(-2.20717975660666E-5,-0.00500000001630823,
-0.00099152216154249));
#3157=CARTESIAN_POINT('Ctrl Pts',(-1.47292366074848E-5,-0.0050000000158632,
-0.000991512476727336));
#3158=CARTESIAN_POINT('Ctrl Pts',(-7.3866655541157E-6,-0.00500000001541243,
-0.000991508546376759));
#3159=CARTESIAN_POINT('Ctrl Pts',(-4.4092249370988E-8,-0.00500000001495753,
-0.000991510350975005));
#3160=CARTESIAN_POINT('Ctrl Pts',(0.000482813204058313,-0.00499999998504277,
-0.000991629023733715));
#3161=CARTESIAN_POINT('Ctrl Pts',(0.000965646141812395,-0.005,-0.00101681337172211));
#3162=CARTESIAN_POINT('Ctrl Pts',(0.00144719332304809,-0.005,-0.0010621702020272));
#3163=CARTESIAN_POINT('Ctrl Pts',(0.00192874050428379,-0.005,-0.00110752703233228));
#3164=CARTESIAN_POINT('Ctrl Pts',(0.00240902445338621,-0.005,-0.00117308198576979));
#3165=CARTESIAN_POINT('Ctrl Pts',(0.00288673400514377,-0.005,-0.00125470818580277));
#3166=CARTESIAN_POINT('',(0.00288675134594813,-0.005,0.0025534180126148));
#3167=CARTESIAN_POINT('',(0.00288675134594813,-0.005,0.003));
#3168=CARTESIAN_POINT('',(0.,-0.005,0.003));
#3169=CARTESIAN_POINT('Ctrl Pts',(-6.35714439048776E-18,-0.005,0.003));
#3170=CARTESIAN_POINT('Ctrl Pts',(0.00133974596216047,-0.005,0.003));
#3171=CARTESIAN_POINT('Ctrl Pts',(0.00288675134596023,-0.005,0.00255341801261131));
#3172=CARTESIAN_POINT('Ctrl Pts',(-0.00288675134596022,-0.005,0.00255341801261131));
#3173=CARTESIAN_POINT('Ctrl Pts',(-0.00133974596216048,-0.005,0.003));
#3174=CARTESIAN_POINT('Ctrl Pts',(-6.35714439048776E-18,-0.005,0.003));
#3175=CARTESIAN_POINT('Origin',(0.00433012701892219,-0.0025,0.003));
#3176=CARTESIAN_POINT('',(0.00577349577362418,-2.97524702184282E-9,-0.00125468783280786));
#3177=CARTESIAN_POINT('Ctrl Pts',(0.00288675654646057,-0.00499999099244824,
-0.00125466787888762));
#3178=CARTESIAN_POINT('Ctrl Pts',(0.0031255993689597,-0.00458630308885659,
-0.00117290882464094));
#3179=CARTESIAN_POINT('Ctrl Pts',(0.00336571418606296,-0.00417041202041241,
-0.00110698452667517));
#3180=CARTESIAN_POINT('Ctrl Pts',(0.00360648916145779,-0.00375337754104141,
-0.00106159956055563));
#3181=CARTESIAN_POINT('Ctrl Pts',(0.00384362185895275,-0.00334265167187877,
-0.0010169011469269));
#3182=CARTESIAN_POINT('Ctrl Pts',(0.00408139429007746,-0.00293081781202513,
-0.000992145259800431));
#3183=CARTESIAN_POINT('Ctrl Pts',(0.00431917052189824,-0.0025189772413838,
-0.000991520603317827));
#3184=CARTESIAN_POINT('Ctrl Pts',(0.00432282268426734,-0.00251265150973835,
-0.00099151100880587));
#3185=CARTESIAN_POINT('Ctrl Pts',(0.00432647485050128,-0.00250632577138726,
-0.000991507108820988));
#3186=CARTESIAN_POINT('Ctrl Pts',(0.00433012701679626,-0.00250000003292203,
-0.00099150888414753));
#3187=CARTESIAN_POINT('Ctrl Pts',(0.00457155567050903,-0.00208183327980953,
-0.00099162624317837));
#3188=CARTESIAN_POINT('Ctrl Pts',(0.00481296724285258,-0.00166369620021464,
-0.00101680902829732));
#3189=CARTESIAN_POINT('Ctrl Pts',(0.00505373559306524,-0.00124667318479177,
-0.00106216623675383));
#3190=CARTESIAN_POINT('Ctrl Pts',(0.00529450394327791,-0.000829650169368892,
-0.00110752344521035));
#3191=CARTESIAN_POINT('Ctrl Pts',(0.00553464028677118,-0.00041372182169474,
-0.00117308056855006));
#3192=CARTESIAN_POINT('Ctrl Pts',(0.00577349405586451,-1.4958045768121E-8,
-0.00125470778672835));
#3193=CARTESIAN_POINT('',(0.00577350269189626,2.60208521396521E-18,0.0025534180126148));
#3194=CARTESIAN_POINT('',(0.00577350269189626,2.60208521396521E-18,0.003));
#3195=CARTESIAN_POINT('',(0.00433012701892219,-0.0025,0.003));
#3196=CARTESIAN_POINT('Ctrl Pts',(0.00577350269190231,1.04782842238321E-14,
0.00255341801261131));
#3197=CARTESIAN_POINT('Ctrl Pts',(0.00500000000000243,-0.0013397459621514,
0.003));
#3198=CARTESIAN_POINT('Ctrl Pts',(0.00433012701892219,-0.0025,0.003));
#3199=CARTESIAN_POINT('Ctrl Pts',(0.00433012701892219,-0.0025,0.003));
#3200=CARTESIAN_POINT('Ctrl Pts',(0.00366025403784196,-0.0036602540378486,
0.003));
#3201=CARTESIAN_POINT('Ctrl Pts',(0.00288675134594208,-0.00500000000001048,
0.00255341801261131));
#3202=CARTESIAN_POINT('Origin',(0.00433012701892219,0.0025,0.003));
#3203=CARTESIAN_POINT('Ctrl Pts',(0.00577349749138385,9.00755172443538E-9,
-0.00125466787888738));
#3204=CARTESIAN_POINT('Ctrl Pts',(0.00553465466888475,0.000413696911143324,
-0.00117290882464032));
#3205=CARTESIAN_POINT('Ctrl Pts',(0.00529453984695666,0.000829587976801907,
-0.00110698452667446));
#3206=CARTESIAN_POINT('Ctrl Pts',(0.00505376488126474,0.00124662246177494,
-0.00106159956055527));
#3207=CARTESIAN_POINT('Ctrl Pts',(0.00481663219332591,0.00165734833645487,
-0.00101690114692689));
#3208=CARTESIAN_POINT('Ctrl Pts',(0.00457885982411642,0.00206918223205527,
-0.000992145259800432));
#3209=CARTESIAN_POINT('Ctrl Pts',(0.00434108354354234,0.00248102277454886,
-0.000991520603317914));
#3210=CARTESIAN_POINT('Ctrl Pts',(0.00433743138042441,0.00248734850576197,
-0.000991511008805958));
#3211=CARTESIAN_POINT('Ctrl Pts',(0.00433377921343164,0.00249367424367496,
-0.000991507108821077));
#3212=CARTESIAN_POINT('Ctrl Pts',(0.00433012704637054,0.00249999998169787,
-0.00099150888414762));
#3213=CARTESIAN_POINT('Ctrl Pts',(0.00408869834201345,0.00291816670557086,
-0.000991626243178547));
#3214=CARTESIAN_POINT('Ctrl Pts',(0.00384728679499182,0.00333630379978535,
-0.00101680902829748));
#3215=CARTESIAN_POINT('Ctrl Pts',(0.00360651844477915,0.00375332681520823,
-0.00106216623675393));
#3216=CARTESIAN_POINT('Ctrl Pts',(0.00336575009456648,0.0041703498306311,
-0.00110752344521037));
#3217=CARTESIAN_POINT('Ctrl Pts',(0.0031256137510732,0.00458627817830528,
-0.00117308056854995));
#3218=CARTESIAN_POINT('Ctrl Pts',(0.00288675998197988,0.00499998504195424,
-0.00125470778672829));
#3219=CARTESIAN_POINT('',(0.00433012701892219,0.0025,0.003));
#3220=CARTESIAN_POINT('Ctrl Pts',(0.00288675134594208,0.00500000000001047,
0.00255341801261131));
#3221=CARTESIAN_POINT('Ctrl Pts',(0.00366025403784195,0.0036602540378486,
0.003));
#3222=CARTESIAN_POINT('Ctrl Pts',(0.00433012701892219,0.00250000000000001,
0.003));
#3223=CARTESIAN_POINT('Ctrl Pts',(0.00433012701892219,0.00250000000000001,
0.003));
#3224=CARTESIAN_POINT('Ctrl Pts',(0.00500000000000243,0.00133974596215141,
0.003));
#3225=CARTESIAN_POINT('Ctrl Pts',(0.0057735026919023,-1.04731475701905E-14,
0.00255341801261131));
#3226=CARTESIAN_POINT('Origin',(0.,-8.67361737988404E-19,0.003));
#3227=CARTESIAN_POINT('Origin',(0.,0.,0.003));
#3228=CARTESIAN_POINT('Origin',(0.,0.,0.003));
#3229=CARTESIAN_POINT('Origin',(0.,0.,0.003));
#3230=CARTESIAN_POINT('Origin',(0.,0.,0.003));
#3231=CARTESIAN_POINT('Origin',(0.,0.,0.003));
#3232=CARTESIAN_POINT('Origin',(0.,0.,0.003));
#3233=CARTESIAN_POINT('',(-0.003,-2.16854331959017E-19,0.003));
#3234=CARTESIAN_POINT('Origin',(0.,1.50539707785189E-19,0.003));
#3235=CARTESIAN_POINT('Origin',(0.,1.50539707785189E-19,0.003));
#3236=CARTESIAN_POINT('',(-0.0024585,-1.50539707785188E-19,0.0024585));
#3237=CARTESIAN_POINT('',(0.0024585,-1.50539707785188E-19,0.0024585));
#3238=CARTESIAN_POINT('Origin',(0.,1.50539707785189E-19,0.0024585));
#3239=CARTESIAN_POINT('',(0.0024585,1.50539707785189E-19,-0.0024585));
#3240=CARTESIAN_POINT('',(0.0024585,-1.50539707785188E-19,0.003));
#3241=CARTESIAN_POINT('Origin',(0.,1.50539707785189E-19,-0.0024585));
#3242=CARTESIAN_POINT('Origin',(0.,1.50539707785189E-19,0.0024585));
#3243=CARTESIAN_POINT('Origin',(0.,-8.67361737988404E-19,-0.003));
#3244=CARTESIAN_POINT('',(-0.00653289983773083,-8.00049487542732E-19,-0.003));
#3245=CARTESIAN_POINT('Origin',(0.,0.,-0.003));
#3246=CARTESIAN_POINT('',(0.003,1.50539707785189E-19,-0.003));
#3247=CARTESIAN_POINT('Origin',(0.,1.50539707785189E-19,-0.003));
#3248=CARTESIAN_POINT('Origin',(0.,0.,0.003));
#3249=CARTESIAN_POINT('Origin',(0.,0.,0.003));
#3250=CARTESIAN_POINT('Origin',(0.,0.,0.003));
#3251=CARTESIAN_POINT('Origin',(0.,0.,0.003));
#3252=CARTESIAN_POINT('Origin',(0.,0.,0.003));
#3253=CARTESIAN_POINT('Origin',(0.,0.,0.003));
#3254=CARTESIAN_POINT('Origin',(0.,0.,-0.0019));
#3255=CARTESIAN_POINT('',(-0.00672685951651014,-8.23802697520806E-19,-0.0019));
#3256=CARTESIAN_POINT('',(0.00672685951651014,-8.23802697520806E-19,-0.0019));
#3257=CARTESIAN_POINT('Origin',(0.,0.,-0.0019));
#3258=CARTESIAN_POINT('',(0.00609857484991769,3.11891280187063E-18,-0.00167132308271448));
#3259=CARTESIAN_POINT('',(0.00672685951651014,-8.23802697520806E-19,-0.0019));
#3260=CARTESIAN_POINT('',(0.00304928972140457,-0.00528151667910899,-0.0016713222184328));
#3261=CARTESIAN_POINT('Ctrl Pts',(0.00609857484991769,3.11891280187063E-18,
-0.00167132308271448));
#3262=CARTESIAN_POINT('Ctrl Pts',(0.00558687214450671,-0.000866849236070623,
-0.0014850785291514));
#3263=CARTESIAN_POINT('Ctrl Pts',(0.00455446054479797,-0.00262062618811301,
-0.00124956471272418));
#3264=CARTESIAN_POINT('Ctrl Pts',(0.00354470751944995,-0.00440396020586821,
-0.00148486875055949));
#3265=CARTESIAN_POINT('Ctrl Pts',(0.00304928972140457,-0.00528151667910899,
-0.0016713222184328));
#3266=CARTESIAN_POINT('',(-0.0030492825755407,-0.00528152070006659,-0.00167132218542784));
#3267=CARTESIAN_POINT('Ctrl Pts',(0.00304928742495884,-0.00528152074690959,
-0.00167132308271448));
#3268=CARTESIAN_POINT('Ctrl Pts',(0.00204272414259244,-0.00527179783765308,
-0.00148507881225216));
#3269=CARTESIAN_POINT('Ctrl Pts',(7.63893803576974E-6,-0.00525459158075091,
-0.00124956384220061));
#3270=CARTESIAN_POINT('Ctrl Pts',(-0.00204159528234752,-0.00527178693758448,
-0.00148487017016737));
#3271=CARTESIAN_POINT('Ctrl Pts',(-0.0030492825755407,-0.00528152070006659,
-0.00167132218542784));
#3272=CARTESIAN_POINT('',(-0.00609857240894841,-4.13512055109264E-9,-0.00167132219427486));
#3273=CARTESIAN_POINT('Ctrl Pts',(-0.00304928742495884,-0.00528152074690959,
-0.00167132308271448));
#3274=CARTESIAN_POINT('Ctrl Pts',(-0.00354414953194165,-0.00440494858680314,
-0.0014850785291514));
#3275=CARTESIAN_POINT('Ctrl Pts',(-0.00454675910347703,-0.00263396547651549,
-0.00124956471780991));
#3276=CARTESIAN_POINT('Ctrl Pts',(-0.00558629513036661,-0.000867826734172135,
-0.00148486874039706));
#3277=CARTESIAN_POINT('Ctrl Pts',(-0.00609857240894841,-4.13512055109264E-9,
-0.00167132219427486));
#3278=CARTESIAN_POINT('',(-0.00304928975931557,0.00528151661195546,-0.00167132220416477));
#3279=CARTESIAN_POINT('Ctrl Pts',(-0.00609857484991769,-1.32997605555308E-18,
-0.00167132308271448));
#3280=CARTESIAN_POINT('Ctrl Pts',(-0.00558687214450671,0.000866849236070624,
-0.0014850785291514));
#3281=CARTESIAN_POINT('Ctrl Pts',(-0.00455446055796522,0.00262062616574556,
-0.00124956471572788));
#3282=CARTESIAN_POINT('Ctrl Pts',(-0.00354470754520648,0.00440396016037937,
-0.0014848687445574));
#3283=CARTESIAN_POINT('Ctrl Pts',(-0.00304928975931557,0.00528151661195546,
-0.00167132220416477));
#3284=CARTESIAN_POINT('',(0.00304928284936602,0.00528152070271162,-0.00167132223609364));
#3285=CARTESIAN_POINT('Ctrl Pts',(-0.00304928742495884,0.00528152074690959,
-0.00167132308271448));
#3286=CARTESIAN_POINT('Ctrl Pts',(-0.00204272105198998,0.00527179780779938,
-0.0014850782403984));
#3287=CARTESIAN_POINT('Ctrl Pts',(-7.76376136486891E-6,0.00525459167257932,
-0.00124956559263654));
#3288=CARTESIAN_POINT('Ctrl Pts',(0.00204157993816983,0.0052717867891337,
-0.00148486731803956));
#3289=CARTESIAN_POINT('Ctrl Pts',(0.00304928284936602,0.00528152070271161,
-0.00167132223609364));
#3290=CARTESIAN_POINT('Ctrl Pts',(0.00304928742495884,0.00528152074690959,
-0.00167132308271448));
#3291=CARTESIAN_POINT('Ctrl Pts',(0.00354414953194165,0.00440494858680314,
-0.0014850785291514));
#3292=CARTESIAN_POINT('Ctrl Pts',(0.00454675915627546,0.00263396538325374,
-0.00124956470540752));
#3293=CARTESIAN_POINT('Ctrl Pts',(0.00558629523985264,0.000867826548158844,
-0.00148486876517975));
#3294=CARTESIAN_POINT('Ctrl Pts',(0.00609857257081076,3.86091785822701E-9,
-0.00167132225318787));
#3295=CARTESIAN_POINT('Origin',(0.,0.,-0.0019));
#3296=CARTESIAN_POINT('Origin',(0.,0.,-0.00243289983773083));
#3297=CARTESIAN_POINT('Origin',(-0.00653289983773083,-8.00049487542732E-19,
-0.00243289983773083));
#3298=CARTESIAN_POINT('Ctrl Pts',(-0.003392439652522,-0.005,-0.00134712277563101));
#3299=CARTESIAN_POINT('Ctrl Pts',(-0.00333573810031697,-0.00500000000000045,
-0.00163882427808492));
#3300=CARTESIAN_POINT('Ctrl Pts',(-0.00331969537168416,-0.00528446061132124,
-0.0017230905910049));
#3301=CARTESIAN_POINT('Ctrl Pts',(-0.00229932400794017,-0.005,-0.00113489737894972));
#3302=CARTESIAN_POINT('Ctrl Pts',(-0.0022699050095138,-0.00499999999999817,
-0.00142291384616243));
#3303=CARTESIAN_POINT('Ctrl Pts',(-0.00224289728430885,-0.00527390094042643,
-0.00151087013501245));
#3304=CARTESIAN_POINT('Ctrl Pts',(-3.29902936623155E-5,-0.005,-0.000850450941742578));
#3305=CARTESIAN_POINT('Ctrl Pts',(-3.26547606719844E-5,-0.00500000000000031,
-0.00112590779668));
#3306=CARTESIAN_POINT('Ctrl Pts',(-3.20185584867946E-5,-0.00525319396056387,
-0.00122643947342924));
#3307=CARTESIAN_POINT('Ctrl Pts',(0.00227701681215951,-0.005,-0.00112983249758146));
#3308=CARTESIAN_POINT('Ctrl Pts',(0.0022484543593711,-0.00500000000000123,
-0.0014177910180656));
#3309=CARTESIAN_POINT('Ctrl Pts',(0.0022208841466116,-0.00527363946899514,
-0.00150580534047564));
#3310=CARTESIAN_POINT('Ctrl Pts',(0.00339967250829873,-0.005,-0.00134857200053328));
#3311=CARTESIAN_POINT('Ctrl Pts',(0.00334288426086359,-0.00499999999999969,
-0.00164032138951496));
#3312=CARTESIAN_POINT('Ctrl Pts',(0.00332681896068871,-0.00528453549253266,
-0.00172453975783402));
#3313=CARTESIAN_POINT('Ctrl Pts',(-0.00288675134474064,-0.00500000000209144,
-0.00125471073847394));
#3314=CARTESIAN_POINT('Ctrl Pts',(-0.00288674885929026,-0.00500000430701771,
-0.00129742470408534));
#3315=CARTESIAN_POINT('Ctrl Pts',(-0.0028905782962394,-0.00500664507750752,
-0.00133965873446181));
#3316=CARTESIAN_POINT('Ctrl Pts',(-0.00290550747687201,-0.00503251662150569,
-0.00142447556160194));
#3317=CARTESIAN_POINT('Ctrl Pts',(-0.00291718276997192,-0.00505274378233935,
-0.00146593997083388));
#3318=CARTESIAN_POINT('Ctrl Pts',(-0.00294546681020174,-0.00510173821438759,
-0.00153843965802242));
#3319=CARTESIAN_POINT('Ctrl Pts',(-0.00296171097744791,-0.00512987415389936,
-0.00156974178652319));
#3320=CARTESIAN_POINT('Ctrl Pts',(-0.0029973641746807,-0.00519162567101304,
-0.00162283860847082));
#3321=CARTESIAN_POINT('Ctrl Pts',(-0.00301673813899042,-0.00522515254326503,
-0.00164476243573887));
#3322=CARTESIAN_POINT('Ctrl Pts',(-0.00304109722867609,-0.00526739574704128,
-0.00166516341250573));
#3323=CARTESIAN_POINT('Ctrl Pts',(-0.00304517979804077,-0.00527442761521776,
-0.00166834117515565));
#3324=CARTESIAN_POINT('Ctrl Pts',(-0.00304927734467971,-0.00528152350994555,
-0.00167132319559009));
#3325=CARTESIAN_POINT('Ctrl Pts',(0.00288675134836161,-0.005,-0.00125471114924454));
#3326=CARTESIAN_POINT('Ctrl Pts',(0.00288675631766473,-0.00500000000000004,
-0.0012974247085572));
#3327=CARTESIAN_POINT('Ctrl Pts',(0.00289059260464713,-0.00500663665536417,
-0.00133965834108164));
#3328=CARTESIAN_POINT('Ctrl Pts',(0.00290553325389396,-0.00503250117827399,
-0.00142447487127839));
#3329=CARTESIAN_POINT('Ctrl Pts',(0.00291721280449157,-0.00505272579460931,
-0.00146593933455075));
#3330=CARTESIAN_POINT('Ctrl Pts',(0.00294550149281011,-0.00510171820329803,
-0.00153843998343925));
#3331=CARTESIAN_POINT('Ctrl Pts',(0.00296174628749688,-0.00512985479605879,
-0.00156974282086848));
#3332=CARTESIAN_POINT('Ctrl Pts',(0.00299740088796859,-0.00519161200494954,
-0.00162284327160921));
#3333=CARTESIAN_POINT('Ctrl Pts',(0.00301675173212757,-0.00522515852632879,
-0.00164476913325231));
#3334=CARTESIAN_POINT('Ctrl Pts',(0.00304115183935638,-0.0052673686443409,
-0.0016651647029104));
#3335=CARTESIAN_POINT('Ctrl Pts',(0.0030452057973953,-0.00527442968077303,
-0.00166834749076532));
#3336=CARTESIAN_POINT('Ctrl Pts',(0.00304929520196274,-0.00528151399743187,
-0.00167132436916548));
#3337=CARTESIAN_POINT('Ctrl Pts',(0.00263483093370536,-0.00543633895346819,
-0.00134676459092806));
#3338=CARTESIAN_POINT('Ctrl Pts',(0.00266316771268226,-0.00538725821255638,
-0.00163845434397486));
#3339=CARTESIAN_POINT('Ctrl Pts',(0.00291752191368072,-0.00551558485545108,
-0.00172273174639874));
#3340=CARTESIAN_POINT('Ctrl Pts',(0.00318111242344103,-0.00449015165801158,
-0.00113472996117616));
#3341=CARTESIAN_POINT('Ctrl Pts',(0.00319582542346177,-0.0044646679944478,
-0.00142273422129603));
#3342=CARTESIAN_POINT('Ctrl Pts',(0.0034465028211626,-0.00457825537721831,
-0.00151070202086737));
#3343=CARTESIAN_POINT('Ctrl Pts',(0.00431379023378606,-0.00252829614188812,
-0.000850609795627995));
#3344=CARTESIAN_POINT('Ctrl Pts',(0.0043139544793176,-0.00252801166028083,
-0.00112606891836143));
#3345=CARTESIAN_POINT('Ctrl Pts',(0.004533552476125,-0.00265406372898638,
-0.00122659749600334));
#3346=CARTESIAN_POINT('Ctrl Pts',(0.00546798881062717,-0.000529165564775629,
-0.00112968126622273));
#3347=CARTESIAN_POINT('Ctrl Pts',(0.00545370297731455,-0.000553909353901215,
-0.00141762786335003));
#3348=CARTESIAN_POINT('Ctrl Pts',(0.00567690587397405,-0.000714562699553637,
-0.00150565341172077));
#3349=CARTESIAN_POINT('Ctrl Pts',(0.00602900688720259,0.000442546247817572,
-0.00134819896772613));
#3350=CARTESIAN_POINT('Ctrl Pts',(0.00600062712586943,0.000393391059281772,
-0.00163993606431589));
#3351=CARTESIAN_POINT('Ctrl Pts',(0.00623899133084267,0.00023722070282916,
-0.00172416606619949));
#3352=CARTESIAN_POINT('Ctrl Pts',(0.00577350269307922,2.04894862976534E-12,
-0.00125471073846544));
#3353=CARTESIAN_POINT('Ctrl Pts',(0.00577350515313831,4.26299629761274E-9,
-0.00129742442899938));
#3354=CARTESIAN_POINT('Ctrl Pts',(0.00578117082891029,8.21840813862419E-9,
-0.00133965819483664));
#3355=CARTESIAN_POINT('Ctrl Pts',(0.00581104059525994,1.48736200446331E-8,
-0.00142447497135105));
#3356=CARTESIAN_POINT('Ctrl Pts',(0.0058343954932902,1.73291284348548E-8,
-0.00146593954554163));
#3357=CARTESIAN_POINT('Ctrl Pts',(0.00589096860070516,1.98232300879166E-8,
-0.00153844019638302));
#3358=CARTESIAN_POINT('Ctrl Pts',(0.00592345795588389,1.99306575175446E-8,
-0.00156974296557482));
#3359=CARTESIAN_POINT('Ctrl Pts',(0.00599476839181334,1.91240807789401E-8,
-0.00162284326885734));
#3360=CARTESIAN_POINT('Ctrl Pts',(0.0060334956968563,4.3290744554038E-9,
-0.00164476902601384));
#3361=CARTESIAN_POINT('Ctrl Pts',(0.00608225115690581,3.0134882409869E-8,
-0.00166516477388993));
#3362=CARTESIAN_POINT('Ctrl Pts',(0.00609039298841603,1.06347343117895E-8,
-0.00166834748495594));
#3363=CARTESIAN_POINT('Ctrl Pts',(0.00609857319807417,1.00115177371027E-8,
-0.00167132447137854));
#3364=CARTESIAN_POINT('Ctrl Pts',(-0.00602542310434739,0.000436338953829055,
-0.00134676459100889));
#3365=CARTESIAN_POINT('Ctrl Pts',(-0.005997086325367,0.000387258212911715,
-0.00163845434406099));
#3366=CARTESIAN_POINT('Ctrl Pts',(-0.00623539755860201,0.000231144334731493,
-0.00172273174648082));
#3367=CARTESIAN_POINT('Ctrl Pts',(-0.00547914161454391,-0.000509848341744993,
-0.00113472996121131));
#3368=CARTESIAN_POINT('Ctrl Pts',(-0.00546442861452444,-0.000535332005308533,
-0.0014227342213371));
#3369=CARTESIAN_POINT('Ctrl Pts',(-0.00568813687240654,-0.00069563130849836,
-0.00151070202090343));
#3370=CARTESIAN_POINT('Ctrl Pts',(-0.00434646380406661,-0.00247170385809752,
-0.000850609795590723));
#3371=CARTESIAN_POINT('Ctrl Pts',(-0.00434629955853541,-0.00247198833970446,
-0.001126068918326));
#3372=CARTESIAN_POINT('Ctrl Pts',(-0.004565262850637,-0.00259913974920765,
-0.0012265974959679));
#3373=CARTESIAN_POINT('Ctrl Pts',(-0.00319226522706066,-0.00447083443549553,
-0.00112968126626212));
#3374=CARTESIAN_POINT('Ctrl Pts',(-0.00320655106037197,-0.00444609064636982,
-0.00141762786339413));
#3375=CARTESIAN_POINT('Ctrl Pts',(-0.00345728238725047,-0.00455906335224487,
-0.00150565341176094));
#3376=CARTESIAN_POINT('Ctrl Pts',(-0.00263124715043141,-0.00544254624818199,
-0.00134819896780807));
#3377=CARTESIAN_POINT('Ctrl Pts',(-0.00265962691176801,-0.00539339105964081,
-0.00163993606440357));
#3378=CARTESIAN_POINT('Ctrl Pts',(-0.00291405651026752,-0.00552173533827817,
-0.00172416606628272));
#3379=CARTESIAN_POINT('Ctrl Pts',(-0.00577350269307922,-2.04894842162822E-12,
-0.00125471073846544));
#3380=CARTESIAN_POINT('Ctrl Pts',(-0.00577350515315459,-4.26302450609168E-9,
-0.00129742471201551));
#3381=CARTESIAN_POINT('Ctrl Pts',(-0.00578117093028351,-8.21845998660043E-9,
-0.00133965875175794));
#3382=CARTESIAN_POINT('Ctrl Pts',(-0.00581104091458347,-1.48736587837042E-8,
-0.00142447558130857));
#3383=CARTESIAN_POINT('Ctrl Pts',(-0.00583439578648829,-1.7329148283752E-8,
-0.00146593997989766));
#3384=CARTESIAN_POINT('Ctrl Pts',(-0.00589096826521234,-1.98232085481949E-8,
-0.00153843971092982));
#3385=CARTESIAN_POINT('Ctrl Pts',(-0.00592345684890417,-1.99306575292987E-8,
-0.00156974187766182));
#3386=CARTESIAN_POINT('Ctrl Pts',(-0.00599476195176788,-1.91241658087579E-8,
-0.00162283873325911));
#3387=CARTESIAN_POINT('Ctrl Pts',(-0.00603348400147061,-4.35666052321621E-9,
-0.00164476252292788));
#3388=CARTESIAN_POINT('Ctrl Pts',(-0.00608224747444197,-3.0126263225575E-8,
-0.00166516355117631));
#3389=CARTESIAN_POINT('Ctrl Pts',(-0.0060903782558774,-1.06374662316222E-8,
-0.00166834120404817));
#3390=CARTESIAN_POINT('Ctrl Pts',(-0.00609857222254513,-1.0011591587375E-8,
-0.0016713232114511));
#3391=CARTESIAN_POINT('Ctrl Pts',(0.00602542310430558,-0.00043633895375665,
-0.00134676459099296));
#3392=CARTESIAN_POINT('Ctrl Pts',(0.00599708632532562,-0.000387258212840311,
-0.00163845434404502));
#3393=CARTESIAN_POINT('Ctrl Pts',(0.00623539755856036,-0.000231144334660519,
-0.00172273174646472));
#3394=CARTESIAN_POINT('Ctrl Pts',(0.00547914161451545,0.000509848341794287,
-0.00113472996120278));
#3395=CARTESIAN_POINT('Ctrl Pts',(0.00546442861449691,0.000535332005357402,
-0.00142273422132636));
#3396=CARTESIAN_POINT('Ctrl Pts',(0.00568813687237712,0.000695631308545852,
-0.00151070202089563));
#3397=CARTESIAN_POINT('Ctrl Pts',(0.0043464638040607,0.00247170385810776,
-0.000850609795600803));
#3398=CARTESIAN_POINT('Ctrl Pts',(0.00434629955852742,0.00247198833971471,
-0.00112606891833642));
#3399=CARTESIAN_POINT('Ctrl Pts',(0.00456526285063273,0.00259913974921762,
-0.00122659749597718));
#3400=CARTESIAN_POINT('Ctrl Pts',(0.00319226522710051,0.00447083443542652,
-0.00112968126625049));
#3401=CARTESIAN_POINT('Ctrl Pts',(0.00320655106041276,0.00444609064630528,
-0.0014176278633837));
#3402=CARTESIAN_POINT('Ctrl Pts',(0.00345728238728788,0.00455906335217811,
-0.00150565341175013));
#3403=CARTESIAN_POINT('Ctrl Pts',(0.00263124715047146,0.00544254624811262,
-0.00134819896779255));
#3404=CARTESIAN_POINT('Ctrl Pts',(0.00265962691180747,0.00539339105957097,
-0.00163993606438704));
#3405=CARTESIAN_POINT('Ctrl Pts',(0.00291405651030647,0.00552173533820915,
-0.00172416606626701));
#3406=CARTESIAN_POINT('Ctrl Pts',(0.00288675134479146,0.00500000000200342,
-0.00125471073845639));
#3407=CARTESIAN_POINT('Ctrl Pts',(0.00288674891221946,0.00500000421534183,
-0.00129742433834695));
#3408=CARTESIAN_POINT('Ctrl Pts',(0.00289057833514563,0.00500664479424417,
-0.00133965801827952));
#3409=CARTESIAN_POINT('Ctrl Pts',(0.00290550744416946,0.00503251593448348,
-0.00142447464062012));
#3410=CARTESIAN_POINT('Ctrl Pts',(0.00291718274092557,0.00505274299951618,
-0.00146593914613713));
#3411=CARTESIAN_POINT('Ctrl Pts',(0.0029454671218375,0.00510173791908386,
-0.00153843988171478));
#3412=CARTESIAN_POINT('Ctrl Pts',(0.00296171174464259,0.00512987464416147,
-0.00156974276006984));
#3413=CARTESIAN_POINT('Ctrl Pts',(0.00299736772729687,0.00519163102478694,
-0.00162284319962407));
#3414=CARTESIAN_POINT('Ctrl Pts',(0.00301674403056076,0.00522516248638102,
-0.00164476895368728));
#3415=CARTESIAN_POINT('Ctrl Pts',(0.00304109982315767,0.00526739903835552,
-0.0016651648357756));
#3416=CARTESIAN_POINT('Ctrl Pts',(0.0030451872163614,0.0052744400176427,
-0.00166834735963212));
#3417=CARTESIAN_POINT('Ctrl Pts',(0.00304927788497547,0.00528152402964165,
-0.00167132437123018));
#3418=CARTESIAN_POINT('Ctrl Pts',(-0.00263483093380463,0.00543633895329622,
-0.00134676459088959));
#3419=CARTESIAN_POINT('Ctrl Pts',(-0.00266316771278097,0.0053872582123861,
-0.00163845434394135));
#3420=CARTESIAN_POINT('Ctrl Pts',(-0.00291752191378344,0.00551558485528404,
-0.00172273174636237));
#3421=CARTESIAN_POINT('Ctrl Pts',(-0.00318111242350983,0.00449015165789242,
-0.00113472996115856));
#3422=CARTESIAN_POINT('Ctrl Pts',(-0.00319582542352974,0.00446466799432721,
-0.00142273422128192));
#3423=CARTESIAN_POINT('Ctrl Pts',(-0.00344650282123468,0.00457825537710422,
-0.00151070202085223));
#3424=CARTESIAN_POINT('Ctrl Pts',(-0.00431379023378665,0.00252829614188709,
-0.000850609795645256));
#3425=CARTESIAN_POINT('Ctrl Pts',(-0.00431395447931927,0.00252801166027967,
-0.00112606891838478));
#3426=CARTESIAN_POINT('Ctrl Pts',(-0.00453355247613352,0.00265406372898939,
-0.00122659749602347));
#3427=CARTESIAN_POINT('Ctrl Pts',(-0.00546798881055722,0.000529165564896799,
-0.00112968126620581));
#3428=CARTESIAN_POINT('Ctrl Pts',(-0.00545370297724336,0.000553909354023832,
-0.00141762786333782));
#3429=CARTESIAN_POINT('Ctrl Pts',(-0.0056769058739087,0.000714562699675378,
-0.00150565341170545));
#3430=CARTESIAN_POINT('Ctrl Pts',(-0.00602900688710061,-0.000442546247640928,
-0.0013481989676864));
#3431=CARTESIAN_POINT('Ctrl Pts',(-0.00600062712576853,-0.000393391059106834,
-0.0016399360642808));
#3432=CARTESIAN_POINT('Ctrl Pts',(-0.00623899133074701,-0.000237220702652166,
-0.00172416606616207));
#3433=CARTESIAN_POINT('Ctrl Pts',(-0.00288675134826077,0.005,-0.00125471027324244));
#3434=CARTESIAN_POINT('Ctrl Pts',(-0.00288675621269418,0.00499999999999996,
-0.00129742428190381));
#3435=CARTESIAN_POINT('Ctrl Pts',(-0.00289059247963899,0.00500663678669082,
-0.00133965836278528));
#3436=CARTESIAN_POINT('Ctrl Pts',(-0.00290553316002905,0.00503250164178277,
-0.00142447528722027));
#3437=CARTESIAN_POINT('Ctrl Pts',(-0.00291721269935843,0.00505272634054306,
-0.00146593974202318));
#3438=CARTESIAN_POINT('Ctrl Pts',(-0.00294550107180259,0.00510171830584963,
-0.00153843954266769));
#3439=CARTESIAN_POINT('Ctrl Pts',(-0.00296174544794714,0.00512985417813293,
-0.00156974173146961));
#3440=CARTESIAN_POINT('Ctrl Pts',(-0.00299739728854999,0.00519160657190795,
-0.00162283861855676));
#3441=CARTESIAN_POINT('Ctrl Pts',(-0.00301674558501153,0.00522514801552304,
-0.00164476237777865));
#3442=CARTESIAN_POINT('Ctrl Pts',(-0.00304114956668833,0.00526736597433145,
-0.00166516356742261));
#3443=CARTESIAN_POINT('Ctrl Pts',(-0.00304519818604292,0.00527441693996766,
-0.00166834116596992));
#3444=CARTESIAN_POINT('Ctrl Pts',(-0.00304929469773904,0.00528151354343759,
-0.00167132322067999));
#3445=CARTESIAN_POINT('Ctrl Pts',(0.00338841005797876,0.005,-0.00134634165980086));
#3446=CARTESIAN_POINT('Ctrl Pts',(0.00333176957023632,0.00500000000000039,
-0.00163801755763053));
#3447=CARTESIAN_POINT('Ctrl Pts',(0.00331572633073014,0.00528441681323915,
-0.0017223080413616));
#3448=CARTESIAN_POINT('Ctrl Pts',(0.0022964618679159,0.005,-0.00113452542043072));
#3449=CARTESIAN_POINT('Ctrl Pts',(0.00226702861060034,0.0049999999999983,
-0.00142251516960501));
#3450=CARTESIAN_POINT('Ctrl Pts',(0.00224010467644372,0.00527386950404515,
-0.00151049666360363));
#3451=CARTESIAN_POINT('Ctrl Pts',(3.22883156223924E-5,0.005,-0.000850800421083646));
#3452=CARTESIAN_POINT('Ctrl Pts',(3.19675726731644E-5,0.00500000000000161,
-0.00112626220337184));
#3453=CARTESIAN_POINT('Ctrl Pts',(3.13356900579081E-5,0.00525321490521392,
-0.00122678714678169));
#3454=CARTESIAN_POINT('Ctrl Pts',(-0.00227419770331868,0.005,-0.00112950336234551));
#3455=CARTESIAN_POINT('Ctrl Pts',(-0.00224561484281812,0.00499999999999842,
-0.00141743587027432));
#3456=CARTESIAN_POINT('Ctrl Pts',(-0.00221813611685098,0.00527361024641964,
-0.00150547469000147));
#3457=CARTESIAN_POINT('Ctrl Pts',(-0.00339548924405207,0.005,-0.00134775642748932));
#3458=CARTESIAN_POINT('Ctrl Pts',(-0.00333876378176818,0.00500000000000037,
-0.00163947896049063));
#3459=CARTESIAN_POINT('Ctrl Pts',(-0.0033226983415365,0.00528448991405657,
-0.00172372275338737));
#3460=CARTESIAN_POINT('Origin',(0.,1.50539707785189E-19,-0.003));
#3461=CARTESIAN_POINT('',(0.003,-2.16854331959017E-19,-0.003));
#3462=CARTESIAN_POINT('Origin',(0.,1.50539707785189E-19,0.0024585));
#3463=CARTESIAN_POINT('',(-0.0024585,-1.50539707785188E-19,0.0024585));
#3822=UNCERTAINTY_MEASURE_WITH_UNIT(LENGTH_MEASURE(1.E-5),#3833,
'DISTANCE_ACCURACY_VALUE',
'Maximum model space distance between geometric entities at asserted c
onnectivities');
#3824=UNCERTAINTY_MEASURE_WITH_UNIT(LENGTH_MEASURE(1.E-5),#3833,
'DISTANCE_ACCURACY_VALUE',
'Maximum model space distance between geometric entities at asserted c
onnectivities');
#3830=(
GEOMETRIC_REPRESENTATION_CONTEXT(3)
GLOBAL_UNCERTAINTY_ASSIGNED_CONTEXT((#3822))
GLOBAL_UNIT_ASSIGNED_CONTEXT((#3833,#3834,#3835))
REPRESENTATION_CONTEXT('','3D')
);
#3832=(
GEOMETRIC_REPRESENTATION_CONTEXT(3)
GLOBAL_UNCERTAINTY_ASSIGNED_CONTEXT((#3824))
GLOBAL_UNIT_ASSIGNED_CONTEXT((#3833,#3834,#3835))
REPRESENTATION_CONTEXT('','3D')
);
#3833=(
LENGTH_UNIT()
NAMED_UNIT(*)
SI_UNIT($,.METRE.)
);
#3834=(
NAMED_UNIT(*)
PLANE_ANGLE_UNIT()
SI_UNIT($,.RADIAN.)
);
#3835=(
NAMED_UNIT(*)
SI_UNIT($,.STERADIAN.)
SOLID_ANGLE_UNIT()
);
#3841=SHAPE_DEFINITION_REPRESENTATION(#3848,#3867);
#3848=PRODUCT_DEFINITION_SHAPE('',$,#3875);
#3867=SHAPE_REPRESENTATION('',(#1951),#3830);
#3869=PRODUCT_DEFINITION_CONTEXT('part definition',#3892,'design');
#3875=PRODUCT_DEFINITION('2026-10-07-15-37-59-801',
'Hex flange nut M6x1.00',#3882,#3869);
#3882=PRODUCT_DEFINITION_FORMATION('',$,#3899);
#3892=APPLICATION_CONTEXT(
'Core Data for Automotive Mechanical Design Process');
#3893=PRODUCT_CONTEXT('part definition',#3892,'mechanical');
#3899=PRODUCT('2026-10-07-15-37-59-801','Hex flange nut M6x1.00',
'Hex flange nut M6x1.00',(#3893));
#3905=PRESENTATION_STYLE_ASSIGNMENT((#3911));
#3911=SURFACE_STYLE_USAGE(.BOTH.,#3917);
#3917=SURFACE_SIDE_STYLE('',(#3923));
#3923=SURFACE_STYLE_FILL_AREA(#3929);
#3929=FILL_AREA_STYLE('Opaque(154,165,175)',(#3935));
#3935=FILL_AREA_STYLE_COLOUR('Opaque(154,165,175)',#3941);
#3941=COLOUR_RGB('Opaque(154,165,175)', 0.40784314, 0.44705882, 0.49803922);
ENDSEC;
END-ISO-10303-21;
